ISO-10303-21;
HEADER;
FILE_DESCRIPTION (('STEP AP214'),
    '1' );
FILE_NAME ('link.step',
    '2026-10-11T23:18:24',
    ( '' ),
    ( '' ),
    'SwSTEP 2.0',
    'SolidWorks 2021',
    '' );
FILE_SCHEMA (( 'AUTOMOTIVE_DESIGN' ));
ENDSEC;

DATA;
#6=CIRCLE ( 'NONE', #7892, 1.600000000000000311 ) ;
#16=AXIS2_PLACEMENT_3D ( 'NONE', #3877, #7054, #1824 ) ;
#17=CARTESIAN_POINT ( 'NONE',  ( 2.525608486058770641, 0.09999999999999982514, -2.423076923076923350 ) ) ;
#22=ORIENTED_EDGE ( 'NONE', *, *, #1316, .F. ) ;
#23=FACE_OUTER_BOUND ( 'NONE', #9551, .T. ) ;
#25=ORIENTED_EDGE ( 'NONE', *, *, #7176, .T. ) ;
#26=AXIS2_PLACEMENT_3D ( 'NONE', #4384, #4937, #13276 ) ;
#29=ADVANCED_FACE ( 'NONE', ( #6308 ), #10384, .T. ) ;
#38=ORIENTED_EDGE ( 'NONE', *, *, #5654, .F. ) ;
#65=DIRECTION ( 'NONE',  ( 0.000000000000000000, 0.000000000000000000, 1.000000000000000000 ) ) ;
#81=EDGE_LOOP ( 'NONE', ( #694, #11176, #5108, #897 ) ) ;
#84=( NAMED_UNIT ( * ) SI_UNIT ( $, .STERADIAN. ) SOLID_ANGLE_UNIT ( ) );
#86=CIRCLE ( 'NONE', #7751, 1.600000000000000311 ) ;
#121=VECTOR ( 'NONE', #10076, 1000.000000000000000 ) ;
#123=( NAMED_UNIT ( * ) SI_UNIT ( $, .STERADIAN. ) SOLID_ANGLE_UNIT ( ) );
#181=EDGE_CURVE ( 'NONE', #11338, #1291, #2903, .T. ) ;
#197=EDGE_CURVE ( 'NONE', #3277, #3201, #3548, .T. ) ;
#198=EDGE_CURVE ( 'NONE', #9031, #937, #1143, .T. ) ;
#202=CARTESIAN_POINT ( 'NONE',  ( 0.000000000000000000, 0.09999999999999982514, 0.000000000000000000 ) ) ;
#210=EDGE_CURVE ( 'NONE', #8040, #5490, #481, .T. ) ;
#211=DIRECTION ( 'NONE',  ( 0.000000000000000000, 0.000000000000000000, -1.000000000000000000 ) ) ;
#225=ORIENTED_EDGE ( 'NONE', *, *, #4550, .T. ) ;
#226=FACE_OUTER_BOUND ( 'NONE', #1132, .T. ) ;
#229=DIRECTION ( 'NONE',  ( 1.000000000000000000, 0.000000000000000000, 1.224646799147353207E-16 ) ) ;
#255=ORIENTED_EDGE ( 'NONE', *, *, #3006, .T. ) ;
#275=CARTESIAN_POINT ( 'NONE',  ( 0.000000000000000000, 3.000000000000000000, 3.400000000000001243 ) ) ;
#283=CIRCLE ( 'NONE', #2044, 3.399999999999999911 ) ;
#293=CARTESIAN_POINT ( 'NONE',  ( 0.000000000000000000, 3.000000000000000000, 1.600000000000000311 ) ) ;
#312=AXIS2_PLACEMENT_3D ( 'NONE', #8923, #4738, #13201 ) ;
#323=EDGE_LOOP ( 'NONE', ( #13175, #3374, #10326, #9587 ) ) ;
#325=CARTESIAN_POINT ( 'NONE',  ( 31.00000000000000000, 2.900000000000000355, -3.399999999999999911 ) ) ;
#332=PLANE ( 'NONE',  #905 ) ;
#336=TOROIDAL_SURFACE ( 'NONE', #2968, 3.100000000000000533, 0.1000000000000000056 ) ;
#341=ORIENTED_EDGE ( 'NONE', *, *, #9398, .F. ) ;
#343=DIRECTION ( 'NONE',  ( 0.000000000000000000, 1.000000000000000000, -0.000000000000000000 ) ) ;
#345=AXIS2_PLACEMENT_3D ( 'NONE', #12872, #1435, #8649 ) ;
#350=CARTESIAN_POINT ( 'NONE',  ( 28.47439151394123158, 3.000000000000000000, -2.423076923076924682 ) ) ;
#358=UNCERTAINTY_MEASURE_WITH_UNIT (LENGTH_MEASURE( 1.000000000000000082E-05 ), #5230, 'distance_accuracy_value', 'NONE');
#377=ORIENTED_EDGE ( 'NONE', *, *, #9624, .T. ) ;
#382=CARTESIAN_POINT ( 'NONE',  ( 0.000000000000000000, 0.000000000000000000, 3.400000000000001243 ) ) ;
#384=ORIENTED_EDGE ( 'NONE', *, *, #10954, .T. ) ;
#392=DIRECTION ( 'NONE',  ( 0.000000000000000000, 0.000000000000000000, 1.000000000000000000 ) ) ;
#402=DIRECTION ( 'NONE',  ( 0.000000000000000000, 0.000000000000000000, 1.000000000000000000 ) ) ;
#412=ORIENTED_EDGE ( 'NONE', *, *, #9690, .F. ) ;
#441=DIRECTION ( 'NONE',  ( 0.000000000000000000, 0.000000000000000000, 1.000000000000000000 ) ) ;
#450=CARTESIAN_POINT ( 'NONE',  ( 0.000000000000000000, 0.000000000000000000, 0.000000000000000000 ) ) ;
#455=DIRECTION ( 'NONE',  ( 0.000000000000000000, 1.000000000000000000, -0.000000000000000000 ) ) ;
#458=EDGE_CURVE ( 'NONE', #7779, #12211, #11592, .T. ) ;
#467=ORIENTED_EDGE ( 'NONE', *, *, #12897, .T. ) ;
#481=CIRCLE ( 'NONE', #6643, 0.1000000000000000472 ) ;
#493=CIRCLE ( 'NONE', #9944, 3.399999999999999911 ) ;
#517=DIRECTION ( 'NONE',  ( -0.000000000000000000, -1.000000000000000000, -0.000000000000000000 ) ) ;
#537=ADVANCED_FACE ( 'NONE', ( #23 ), #13587, .F. ) ;
#538=DIRECTION ( 'NONE',  ( 8.881784197001252323E-16, 0.000000000000000000, 1.000000000000000000 ) ) ;
#541=AXIS2_PLACEMENT_3D ( 'NONE', #13133, #7884, #11067 ) ;
#548=CIRCLE ( 'NONE', #5169, 1.500000000000003997 ) ;
#552=DIRECTION ( 'NONE',  ( 0.000000000000000000, 0.000000000000000000, 1.000000000000000000 ) ) ;
#553=CIRCLE ( 'NONE', #1211, 3.500000000000000888 ) ;
#574=CARTESIAN_POINT ( 'NONE',  ( 4.690415759823430619, 2.900000000000000355, -4.500000000000000888 ) ) ;
#576=CARTESIAN_POINT ( 'NONE',  ( 0.000000000000000000, 2.900000000000000355, 0.000000000000000000 ) ) ;
#594=VERTEX_POINT ( 'NONE', #2556 ) ;
#626=ORIENTED_EDGE ( 'NONE', *, *, #9282, .F. ) ;
#630=ORIENTED_EDGE ( 'NONE', *, *, #11392, .T. ) ;
#636=CARTESIAN_POINT ( 'NONE',  ( 4.690415759823430619, 0.09999999999999982514, 4.500000000000000888 ) ) ;
#645=CARTESIAN_POINT ( 'NONE',  ( 31.00000000000000000, 3.000000000000000000, 0.000000000000000000 ) ) ;
#665=AXIS2_PLACEMENT_3D ( 'NONE', #9357, #12667, #2244 ) ;
#671=ORIENTED_EDGE ( 'NONE', *, *, #13142, .F. ) ;
#685=CARTESIAN_POINT ( 'NONE',  ( 28.47439151394123158, 2.900000000000000355, 2.423076923076924238 ) ) ;
#694=ORIENTED_EDGE ( 'NONE', *, *, #5265, .T. ) ;
#698=DIRECTION ( 'NONE',  ( 0.000000000000000000, 1.000000000000000000, -0.000000000000000000 ) ) ;
#722=DIRECTION ( 'NONE',  ( 1.000000000000000000, 0.000000000000000000, 0.000000000000000000 ) ) ;
#727=ORIENTED_EDGE ( 'NONE', *, *, #4626, .T. ) ;
#749=AXIS2_PLACEMENT_3D ( 'NONE', #1426, #5473, #4586 ) ;
#761=CIRCLE ( 'NONE', #2511, 1.500000000000000222 ) ;
#790=CARTESIAN_POINT ( 'NONE',  ( 0.000000000000000000, 2.900000000000000355, 3.400000000000001243 ) ) ;
#804=ORIENTED_EDGE ( 'NONE', *, *, #12412, .F. ) ;
#837=FACE_OUTER_BOUND ( 'NONE', #2927, .T. ) ;
#850=CARTESIAN_POINT ( 'NONE',  ( 0.000000000000000000, 2.900000000000000355, -1.500000000000000222 ) ) ;
#856=CARTESIAN_POINT ( 'NONE',  ( 4.286263797015737088E-16, 3.000000000000000000, 3.500000000000000888 ) ) ;
#864=EDGE_CURVE ( 'NONE', #8802, #6054, #283, .T. ) ;
#882=CIRCLE ( 'NONE', #16, 3.399999999999999911 ) ;
#890=CARTESIAN_POINT ( 'NONE',  ( 31.00000000000000000, 2.900000000000000355, 0.000000000000000000 ) ) ;
#897=ORIENTED_EDGE ( 'NONE', *, *, #5905, .F. ) ;
#898=DIRECTION ( 'NONE',  ( 0.7216024245882196597, 0.000000000000000000, 0.6923076923076926237 ) ) ;
#903=CARTESIAN_POINT ( 'NONE',  ( 0.000000000000000000, 0.09999999999999982514, 0.000000000000000000 ) ) ;
#905=AXIS2_PLACEMENT_3D ( 'NONE', #8919, #11968, #4655 ) ;
#937=VERTEX_POINT ( 'NONE', #12487 ) ;
#943=AXIS2_PLACEMENT_3D ( 'NONE', #4491, #8681, #11656 ) ;
#955=EDGE_CURVE ( 'NONE', #10261, #8040, #6326, .T. ) ;
#956=PRODUCT_CONTEXT ( 'NONE', #1418, 'mechanical' ) ;
#968=DIRECTION ( 'NONE',  ( -0.000000000000000000, -1.000000000000000000, 0.000000000000000000 ) ) ;
#976=CARTESIAN_POINT ( 'NONE',  ( 31.00000000000000000, 2.900000000000000355, 0.000000000000000000 ) ) ;
#997=LINE ( 'NONE', #13463, #7125 ) ;
#1010=CARTESIAN_POINT ( 'NONE',  ( 31.00000000000000000, 0.09999999999999982514, 0.000000000000000000 ) ) ;
#1016=ORIENTED_EDGE ( 'NONE', *, *, #5815, .F. ) ;
#1026=CARTESIAN_POINT ( 'NONE',  ( 28.47439151394123158, 2.900000000000000355, -2.423076923076924682 ) ) ;
#1030=EDGE_CURVE ( 'NONE', #2354, #12940, #6015, .T. ) ;
#1033=EDGE_CURVE ( 'NONE', #6631, #1278, #9301, .T. ) ;
#1034=ORIENTED_EDGE ( 'NONE', *, *, #10476, .T. ) ;
#1035=DIRECTION ( 'NONE',  ( 0.000000000000000000, 0.000000000000000000, 1.000000000000000000 ) ) ;
#1036=SURFACE_SIDE_STYLE ('',( #4266 ) ) ;
#1044=ORIENTED_EDGE ( 'NONE', *, *, #12723, .T. ) ;
#1049=EDGE_CURVE ( 'NONE', #10250, #2353, #8420, .T. ) ;
#1059=EDGE_CURVE ( 'NONE', #2378, #12695, #10874, .T. ) ;
#1066=EDGE_CURVE ( 'NONE', #1278, #9479, #1841, .T. ) ;
#1084=CARTESIAN_POINT ( 'NONE',  ( 31.00000000000000000, 0.09999999999999982514, 0.000000000000000000 ) ) ;
#1093=AXIS2_PLACEMENT_3D ( 'NONE', #10679, #9375, #8321 ) ;
#1095=EDGE_CURVE ( 'NONE', #1291, #11338, #12829, .T. ) ;
#1096=ADVANCED_FACE ( 'NONE', ( #10676 ), #4245, .T. ) ;
#1105=AXIS2_PLACEMENT_3D ( 'NONE', #12702, #10697, #12762 ) ;
#1116=CIRCLE ( 'NONE', #9239, 0.1000000000000001166 ) ;
#1119=DIRECTION ( 'NONE',  ( 0.000000000000000000, 0.000000000000000000, 1.000000000000000000 ) ) ;
#1124=EDGE_CURVE ( 'NONE', #3555, #5490, #86, .T. ) ;
#1132=EDGE_LOOP ( 'NONE', ( #13487, #412, #2430, #1761 ) ) ;
#1143=CIRCLE ( 'NONE', #10825, 0.09999999999999982514 ) ;
#1149=ORIENTED_EDGE ( 'NONE', *, *, #9004, .F. ) ;
#1168=PRESENTATION_STYLE_ASSIGNMENT (( #7377 ) ) ;
#1198=AXIS2_PLACEMENT_3D ( 'NONE', #5757, #8985, #538 ) ;
#1209=AXIS2_PLACEMENT_3D ( 'NONE', #1542, #9929, #1476 ) ;
#1211=AXIS2_PLACEMENT_3D ( 'NONE', #2018, #6213, #2986 ) ;
#1218=AXIS2_PLACEMENT_3D ( 'NONE', #890, #6256, #9422 ) ;
#1225=( GEOMETRIC_REPRESENTATION_CONTEXT ( 3 ) GLOBAL_UNCERTAINTY_ASSIGNED_CONTEXT ( ( #358 ) ) GLOBAL_UNIT_ASSIGNED_CONTEXT ( ( #5230, #6331, #84 ) ) REPRESENTATION_CONTEXT ( 'NONE', 'WORKASPACE' ) );
#1229=EDGE_CURVE ( 'NONE', #5490, #3555, #13488, .T. ) ;
#1231=DIRECTION ( 'NONE',  ( 0.000000000000000000, 0.000000000000000000, -1.000000000000000000 ) ) ;
#1237=VERTEX_POINT ( 'NONE', #2664 ) ;
#1253=CARTESIAN_POINT ( 'NONE',  ( 4.690415759823430619, 3.000000000000000000, 1.500000000000000000 ) ) ;
#1254=DIRECTION ( 'NONE',  ( -1.000000000000000000, 0.000000000000000000, 0.000000000000000000 ) ) ;
#1263=PRODUCT ( 'link', 'link', '', ( #956 ) ) ;
#1273=DIRECTION ( 'NONE',  ( -1.000000000000000000, 0.000000000000000000, 0.000000000000000000 ) ) ;
#1277=ORIENTED_EDGE ( 'NONE', *, *, #11273, .T. ) ;
#1278=VERTEX_POINT ( 'NONE', #8856 ) ;
#1291=VERTEX_POINT ( 'NONE', #3631 ) ;
#1316=EDGE_CURVE ( 'NONE', #2354, #6704, #11356, .T. ) ;
#1319=CARTESIAN_POINT ( 'NONE',  ( 4.225031457058369317E-16, 3.000000000000000000, -3.400000000000001243 ) ) ;
#1340=ORIENTED_EDGE ( 'NONE', *, *, #7634, .T. ) ;
#1351=CARTESIAN_POINT ( 'NONE',  ( 0.000000000000000000, 2.900000000000000355, 1.399999999999999911 ) ) ;
#1391=AXIS2_PLACEMENT_3D ( 'NONE', #11674, #9545, #6166 ) ;
#1394=CYLINDRICAL_SURFACE ( 'NONE', #1105, 3.500000000000000888 ) ;
#1400=CARTESIAN_POINT ( 'NONE',  ( 1.836970198721030181E-16, 0.09999999999999982514, 1.500000000000000222 ) ) ;
#1402=EDGE_LOOP ( 'NONE', ( #8548, #4333, #2553, #7011 ) ) ;
#1414=TOROIDAL_SURFACE ( 'NONE', #10652, 1.600000000000004086, 0.1000000000000000056 ) ;
#1418=APPLICATION_CONTEXT ( 'automotive_design' ) ;
#1423=AXIS2_PLACEMENT_3D ( 'NONE', #9152, #9363, #12411 ) ;
#1425=ORIENTED_EDGE ( 'NONE', *, *, #3705, .F. ) ;
#1426=CARTESIAN_POINT ( 'NONE',  ( 31.00000000000000000, 2.900000000000000355, 0.000000000000000000 ) ) ;
#1431=ADVANCED_FACE ( 'NONE', ( #2640 ), #1832, .T. ) ;
#1432=VECTOR ( 'NONE', #10143, 1000.000000000000000 ) ;
#1435=DIRECTION ( 'NONE',  ( -1.000000000000000000, 0.000000000000000000, -0.000000000000000000 ) ) ;
#1447=EDGE_CURVE ( 'NONE', #8041, #9479, #13283, .T. ) ;
#1469=CARTESIAN_POINT ( 'NONE',  ( 31.00000000000000000, 0.09999999999999982514, 0.000000000000000000 ) ) ;
#1476=DIRECTION ( 'NONE',  ( 0.000000000000000000, 0.000000000000000000, -1.000000000000000000 ) ) ;
#1481=DIRECTION ( 'NONE',  ( 0.000000000000000000, 0.000000000000000000, 1.000000000000000000 ) ) ;
#1484=EDGE_LOOP ( 'NONE', ( #1936, #11700, #6849, #341 ) ) ;
#1491=DIRECTION ( 'NONE',  ( -1.000000000000000000, 0.000000000000000000, 0.000000000000000000 ) ) ;
#1498=ORIENTED_EDGE ( 'NONE', *, *, #2054, .F. ) ;
#1502=CARTESIAN_POINT ( 'NONE',  ( 0.000000000000000000, 0.000000000000000000, 0.000000000000000000 ) ) ;
#1520=ORIENTED_EDGE ( 'NONE', *, *, #10883, .F. ) ;
#1542=CARTESIAN_POINT ( 'NONE',  ( 0.000000000000000000, 2.900000000000000355, -1.399999999999999911 ) ) ;
#1543=EDGE_CURVE ( 'NONE', #7533, #13228, #1801, .T. ) ;
#1547=DIRECTION ( 'NONE',  ( 0.000000000000000000, 0.000000000000000000, 1.000000000000000000 ) ) ;
#1551=CIRCLE ( 'NONE', #9238, 3.499999999999999556 ) ;
#1561=AXIS2_PLACEMENT_3D ( 'NONE', #6857, #455, #6785 ) ;
#1578=CARTESIAN_POINT ( 'NONE',  ( 26.30958424017656938, 0.09999999999999982514, -4.500000000000000888 ) ) ;
#1584=VERTEX_POINT ( 'NONE', #1667 ) ;
#1585=ORIENTED_EDGE ( 'NONE', *, *, #8385, .F. ) ;
#1590=CIRCLE ( 'NONE', #9283, 3.499999999999999556 ) ;
#1601=FACE_OUTER_BOUND ( 'NONE', #9061, .T. ) ;
#1602=DIRECTION ( 'NONE',  ( 0.000000000000000000, 0.000000000000000000, 1.000000000000000000 ) ) ;
#1641=FACE_OUTER_BOUND ( 'NONE', #8618, .T. ) ;
#1646=ORIENTED_EDGE ( 'NONE', *, *, #7221, .T. ) ;
#1647=ADVANCED_FACE ( 'NONE', ( #10123 ), #7992, .T. ) ;
#1659=CARTESIAN_POINT ( 'NONE',  ( 0.000000000000000000, 0.09999999999999982514, 3.400000000000001243 ) ) ;
#1667=CARTESIAN_POINT ( 'NONE',  ( 2.453448243599948952, 0.000000000000000000, 2.353846153846153921 ) ) ;
#1673=( GEOMETRIC_REPRESENTATION_CONTEXT ( 3 ) GLOBAL_UNCERTAINTY_ASSIGNED_CONTEXT ( ( #13299 ) ) GLOBAL_UNIT_ASSIGNED_CONTEXT ( ( #10404, #9299, #10607 ) ) REPRESENTATION_CONTEXT ( 'NONE', 'WORKASPACE' ) );
#1675=CARTESIAN_POINT ( 'NONE',  ( 0.000000000000000000, 0.09999999999999982514, 0.000000000000000000 ) ) ;
#1676=FACE_OUTER_BOUND ( 'NONE', #81, .T. ) ;
#1677=ORIENTED_EDGE ( 'NONE', *, *, #9921, .T. ) ;
#1721=CARTESIAN_POINT ( 'NONE',  ( 4.690415759823430619, 2.900000000000000355, -1.500000000000000000 ) ) ;
#1739=DIRECTION ( 'NONE',  ( 0.000000000000000000, 1.000000000000000000, -0.000000000000000000 ) ) ;
#1744=ORIENTED_EDGE ( 'NONE', *, *, #11206, .T. ) ;
#1758=CARTESIAN_POINT ( 'NONE',  ( 31.00000000000000000, 3.000000000000000000, 0.000000000000000000 ) ) ;
#1759=CARTESIAN_POINT ( 'NONE',  ( 2.525608486058770641, 2.900000000000000355, -2.423076923076923350 ) ) ;
#1761=ORIENTED_EDGE ( 'NONE', *, *, #4678, .F. ) ;
#1766=CARTESIAN_POINT ( 'NONE',  ( 4.690415759823430619, 0.09999999999999982514, 4.500000000000000888 ) ) ;
#1785=CARTESIAN_POINT ( 'NONE',  ( 26.30958424017656938, 0.09999999999999982514, 4.500000000000000888 ) ) ;
#1801=LINE ( 'NONE', #11484, #10201 ) ;
#1821=AXIS2_PLACEMENT_3D ( 'NONE', #903, #7240, #11235 ) ;
#1824=DIRECTION ( 'NONE',  ( 0.000000000000000000, 0.000000000000000000, 1.000000000000000000 ) ) ;
#1828=CARTESIAN_POINT ( 'NONE',  ( 0.000000000000000000, 3.000000000000000000, 0.000000000000000000 ) ) ;
#1832=CYLINDRICAL_SURFACE ( 'NONE', #6028, 3.499999999999999556 ) ;
#1841=CIRCLE ( 'NONE', #10407, 3.400000000000001243 ) ;
#1843=AXIS2_PLACEMENT_3D ( 'NONE', #1828, #6775, #4714 ) ;
#1844=DIRECTION ( 'NONE',  ( 0.000000000000000000, 0.000000000000000000, 1.000000000000000000 ) ) ;
#1860=CARTESIAN_POINT ( 'NONE',  ( 4.690415759823430619, 2.900000000000000355, 1.399999999999999911 ) ) ;
#1878=CARTESIAN_POINT ( 'NONE',  ( 26.30958424017656938, 3.000000000000000000, -4.500000000000000888 ) ) ;
#1880=DIRECTION ( 'NONE',  ( -1.000000000000000000, -0.000000000000000000, -0.000000000000000000 ) ) ;
#1884=ORIENTED_EDGE ( 'NONE', *, *, #8272, .T. ) ;
#1897=DIRECTION ( 'NONE',  ( 1.000000000000000000, -0.000000000000000000, 0.000000000000000000 ) ) ;
#1914=DIRECTION ( 'NONE',  ( 0.7216024245882217691, 0.000000000000000000, -0.6923076923076904032 ) ) ;
#1932=EDGE_CURVE ( 'NONE', #6498, #3264, #2934, .T. ) ;
#1936=ORIENTED_EDGE ( 'NONE', *, *, #3341, .F. ) ;
#1945=DIRECTION ( 'NONE',  ( -0.000000000000000000, -1.000000000000000000, -0.000000000000000000 ) ) ;
#1956=CARTESIAN_POINT ( 'NONE',  ( 26.30958424017656938, 3.000000000000000000, 1.399999999999999911 ) ) ;
#1966=CIRCLE ( 'NONE', #3700, 3.399999999999999911 ) ;
#1985=AXIS2_PLACEMENT_3D ( 'NONE', #7485, #13560, #7289 ) ;
#2004=DIRECTION ( 'NONE',  ( 0.6923076923076927347, 3.129451665637426527E-15, 0.7216024245882196597 ) ) ;
#2015=AXIS2_PLACEMENT_3D ( 'NONE', #6511, #10715, #5464 ) ;
#2018=CARTESIAN_POINT ( 'NONE',  ( 0.000000000000000000, 0.09999999999999982514, 0.000000000000000000 ) ) ;
#2044=AXIS2_PLACEMENT_3D ( 'NONE', #9984, #4819, #8061 ) ;
#2054=EDGE_CURVE ( 'NONE', #13453, #2354, #11308, .T. ) ;
#2055=DIRECTION ( 'NONE',  ( -0.000000000000000000, -1.000000000000000000, 0.000000000000000000 ) ) ;
#2063=CARTESIAN_POINT ( 'NONE',  ( 0.000000000000000000, 3.000000000000000000, 0.000000000000000000 ) ) ;
#2064=AXIS2_PLACEMENT_3D ( 'NONE', #4291, #11862, #3386 ) ;
#2065=TOROIDAL_SURFACE ( 'NONE', #5140, 3.399999999999999911, 0.1000000000000000056 ) ;
#2068=VERTEX_POINT ( 'NONE', #2105 ) ;
#2091=CARTESIAN_POINT ( 'NONE',  ( 2.453448243599949397, 0.1000000000000000056, -2.353846153846154365 ) ) ;
#2105=CARTESIAN_POINT ( 'NONE',  ( 4.690415759823430619, 0.000000000000000000, 1.399999999999999911 ) ) ;
#2106=CARTESIAN_POINT ( 'NONE',  ( 31.00000000000000000, 3.000000000000000000, 0.000000000000000000 ) ) ;
#2112=ORIENTED_EDGE ( 'NONE', *, *, #198, .F. ) ;
#2129=EDGE_LOOP ( 'NONE', ( #9631, #8673, #12095, #3001 ) ) ;
#2134=DIRECTION ( 'NONE',  ( -0.000000000000000000, -1.000000000000000000, -0.000000000000000000 ) ) ;
#2141=EDGE_LOOP ( 'NONE', ( #5853, #2424 ) ) ;
#2170=CARTESIAN_POINT ( 'NONE',  ( 0.000000000000000000, 3.000000000000000000, 0.000000000000000000 ) ) ;
#2175=ORIENTED_EDGE ( 'NONE', *, *, #3801, .F. ) ;
#2177=CARTESIAN_POINT ( 'NONE',  ( 0.000000000000000000, 0.09999999999999982514, 1.600000000000000311 ) ) ;
#2192=ORIENTED_EDGE ( 'NONE', *, *, #5665, .F. ) ;
#2199=AXIS2_PLACEMENT_3D ( 'NONE', #2091, #5252, #4149 ) ;
#2200=LINE ( 'NONE', #350, #9712 ) ;
#2240=CARTESIAN_POINT ( 'NONE',  ( 31.00000000000000000, 0.000000000000000000, 0.000000000000000000 ) ) ;
#2244=DIRECTION ( 'NONE',  ( 0.000000000000000000, 0.000000000000000000, 1.000000000000000000 ) ) ;
#2260=ADVANCED_FACE ( 'NONE', ( #7732 ), #13249, .T. ) ;
#2276=ORIENTED_EDGE ( 'NONE', *, *, #4306, .T. ) ;
#2279=EDGE_CURVE ( 'NONE', #11521, #10836, #6906, .T. ) ;
#2292=DIRECTION ( 'NONE',  ( -0.000000000000000000, -1.000000000000000000, -0.000000000000000000 ) ) ;
#2297=CIRCLE ( 'NONE', #8450, 0.09999999999999982514 ) ;
#2328=DIRECTION ( 'NONE',  ( 0.000000000000000000, 0.000000000000000000, 1.000000000000000000 ) ) ;
#2353=VERTEX_POINT ( 'NONE', #13459 ) ;
#2354=VERTEX_POINT ( 'NONE', #6983 ) ;
#2361=CARTESIAN_POINT ( 'NONE',  ( 4.690415759823430619, 3.000000000000000000, 4.500000000000000888 ) ) ;
#2378=VERTEX_POINT ( 'NONE', #850 ) ;
#2379=EDGE_CURVE ( 'NONE', #594, #3134, #3609, .T. ) ;
#2391=CARTESIAN_POINT ( 'NONE',  ( 31.00000000000000000, 0.09999999999999982514, 3.399999999999999911 ) ) ;
#2424=ORIENTED_EDGE ( 'NONE', *, *, #1124, .T. ) ;
#2427=ORIENTED_EDGE ( 'NONE', *, *, #1095, .T. ) ;
#2430=ORIENTED_EDGE ( 'NONE', *, *, #6041, .T. ) ;
#2446=EDGE_CURVE ( 'NONE', #3500, #6704, #553, .T. ) ;
#2461=ORIENTED_EDGE ( 'NONE', *, *, #3643, .F. ) ;
#2465=ADVANCED_FACE ( 'NONE', ( #9110 ), #13328, .T. ) ;
#2488=VECTOR ( 'NONE', #11981, 1000.000000000000000 ) ;
#2497=CARTESIAN_POINT ( 'NONE',  ( 4.690415759823430619, 3.000000000000000000, -4.500000000000000888 ) ) ;
#2511=AXIS2_PLACEMENT_3D ( 'NONE', #12551, #10542, #11313 ) ;
#2513=CARTESIAN_POINT ( 'NONE',  ( 26.30958424017656938, 3.000000000000000000, 4.500000000000000888 ) ) ;
#2521=VERTEX_POINT ( 'NONE', #293 ) ;
#2525=CARTESIAN_POINT ( 'NONE',  ( 26.30958424017656938, 2.900000000000000355, 1.500000000000000000 ) ) ;
#2535=ORIENTED_EDGE ( 'NONE', *, *, #458, .F. ) ;
#2546=CARTESIAN_POINT ( 'NONE',  ( 0.000000000000000000, 3.000000000000000000, -3.500000000000000888 ) ) ;
#2553=ORIENTED_EDGE ( 'NONE', *, *, #10391, .F. ) ;
#2556=CARTESIAN_POINT ( 'NONE',  ( 4.286263797015737088E-16, 2.900000000000000355, 3.500000000000000888 ) ) ;
#2564=CARTESIAN_POINT ( 'NONE',  ( 31.00000000000000000, 3.000000000000000000, 3.399999999999999911 ) ) ;
#2574=FACE_OUTER_BOUND ( 'NONE', #10870, .T. ) ;
#2576=CARTESIAN_POINT ( 'NONE',  ( 26.30958424017656938, 3.000000000000000000, -1.500000000000000000 ) ) ;
#2577=CARTESIAN_POINT ( 'NONE',  ( 1.836970198721030181E-16, 2.900000000000000355, 1.500000000000000222 ) ) ;
#2581=ADVANCED_FACE ( 'NONE', ( #226 ), #4945, .T. ) ;
#2583=VERTEX_POINT ( 'NONE', #7455 ) ;
#2592=CYLINDRICAL_SURFACE ( 'NONE', #11322, 3.499999999999999556 ) ;
#2612=ORIENTED_EDGE ( 'NONE', *, *, #6570, .F. ) ;
#2635=CARTESIAN_POINT ( 'NONE',  ( 28.54655175640005282, 0.09999999999999982514, -2.353846153846154809 ) ) ;
#2637=DIRECTION ( 'NONE',  ( 0.6923076923076927347, 1.270456495237146852E-16, 0.7216024245882196597 ) ) ;
#2640=FACE_OUTER_BOUND ( 'NONE', #4685, .T. ) ;
#2642=VECTOR ( 'NONE', #8013, 1000.000000000000000 ) ;
#2664=CARTESIAN_POINT ( 'NONE',  ( 31.00000000000000000, 0.09999999999999982514, -3.499999999999999556 ) ) ;
#2670=DIRECTION ( 'NONE',  ( -2.312964634635742267E-15, 0.000000000000000000, 1.000000000000000000 ) ) ;
#2692=PLANE ( 'NONE',  #4507 ) ;
#2704=DIRECTION ( 'NONE',  ( 0.000000000000000000, 0.000000000000000000, -1.000000000000000000 ) ) ;
#2725=AXIS2_PLACEMENT_3D ( 'NONE', #3495, #5496, #8730 ) ;
#2736=AXIS2_PLACEMENT_3D ( 'NONE', #3850, #9073, #8050 ) ;
#2750=DIRECTION ( 'NONE',  ( -1.000000000000000000, 0.000000000000000000, 0.000000000000000000 ) ) ;
#2767=DIRECTION ( 'NONE',  ( 1.000000000000000000, 0.000000000000000000, 1.224646799147353207E-16 ) ) ;
#2774=ORIENTED_EDGE ( 'NONE', *, *, #7448, .T. ) ;
#2776=DIRECTION ( 'NONE',  ( 1.000000000000000000, 0.000000000000000000, 0.000000000000000000 ) ) ;
#2781=DIRECTION ( 'NONE',  ( 0.7216024245882196597, 0.000000000000000000, 0.6923076923076926237 ) ) ;
#2813=DIRECTION ( 'NONE',  ( 1.000000000000000000, 0.000000000000000000, 1.224646799147353207E-16 ) ) ;
#2817=ORIENTED_EDGE ( 'NONE', *, *, #2379, .T. ) ;
#2821=ORIENTED_EDGE ( 'NONE', *, *, #10476, .F. ) ;
#2823=EDGE_CURVE ( 'NONE', #6054, #3238, #1966, .T. ) ;
#2834=CARTESIAN_POINT ( 'NONE',  ( 26.30958424017656938, 2.900000000000000355, -1.399999999999999911 ) ) ;
#2873=ADVANCED_FACE ( 'NONE', ( #11165 ), #5327, .T. ) ;
#2875=CARTESIAN_POINT ( 'NONE',  ( 31.00000000000000000, 0.000000000000000000, 3.399999999999999911 ) ) ;
#2885=DIRECTION ( 'NONE',  ( -0.000000000000000000, -1.000000000000000000, -0.000000000000000000 ) ) ;
#2903=CIRCLE ( 'NONE', #7525, 1.600000000000004086 ) ;
#2905=TOROIDAL_SURFACE ( 'NONE', #8819, 3.400000000000001243, 0.1000000000000000056 ) ;
#2907=ORIENTED_EDGE ( 'NONE', *, *, #6482, .F. ) ;
#2915=AXIS2_PLACEMENT_3D ( 'NONE', #6819, #8951, #11101 ) ;
#2927=EDGE_LOOP ( 'NONE', ( #3180, #5073, #2774, #3352 ) ) ;
#2928=VECTOR ( 'NONE', #7246, 1000.000000000000000 ) ;
#2934=CIRCLE ( 'NONE', #4691, 3.400000000000001243 ) ;
#2941=LINE ( 'NONE', #8039, #7994 ) ;
#2954=AXIS2_PLACEMENT_3D ( 'NONE', #6047, #9344, #4039 ) ;
#2955=ADVANCED_FACE ( 'NONE', ( #5364 ), #9634, .T. ) ;
#2962=ORIENTED_EDGE ( 'NONE', *, *, #955, .F. ) ;
#2968=AXIS2_PLACEMENT_3D ( 'NONE', #574, #7855, #1602 ) ;
#2977=EDGE_CURVE ( 'NONE', #2583, #8871, #4167, .T. ) ;
#2978=DIRECTION ( 'NONE',  ( -0.000000000000000000, -1.000000000000000000, 0.000000000000000000 ) ) ;
#2981=ORIENTED_EDGE ( 'NONE', *, *, #2823, .T. ) ;
#2985=ORIENTED_EDGE ( 'NONE', *, *, #11508, .T. ) ;
#2986=DIRECTION ( 'NONE',  ( 0.000000000000000000, 0.000000000000000000, 1.000000000000000000 ) ) ;
#3001=ORIENTED_EDGE ( 'NONE', *, *, #9490, .T. ) ;
#3004=FACE_OUTER_BOUND ( 'NONE', #10795, .T. ) ;
#3006=EDGE_CURVE ( 'NONE', #3264, #2583, #3068, .T. ) ;
#3015=ORIENTED_EDGE ( 'NONE', *, *, #12897, .F. ) ;
#3037=CARTESIAN_POINT ( 'NONE',  ( 31.00000000000000000, 3.000000000000000000, 0.000000000000000000 ) ) ;
#3042=ORIENTED_EDGE ( 'NONE', *, *, #13411, .T. ) ;
#3065=DIRECTION ( 'NONE',  ( 0.000000000000000000, 0.000000000000000000, 1.000000000000000000 ) ) ;
#3068=CIRCLE ( 'NONE', #12753, 3.400000000000001243 ) ;
#3081=DIRECTION ( 'NONE',  ( 1.000000000000000000, 0.000000000000000000, 0.000000000000000000 ) ) ;
#3085=CIRCLE ( 'NONE', #12981, 0.1000000000000001166 ) ;
#3103=DIRECTION ( 'NONE',  ( -0.000000000000000000, -1.000000000000000000, -0.000000000000000000 ) ) ;
#3105=ORIENTED_EDGE ( 'NONE', *, *, #4072, .F. ) ;
#3113=EDGE_CURVE ( 'NONE', #6069, #10836, #6586, .T. ) ;
#3126=CARTESIAN_POINT ( 'NONE',  ( 26.30958424017656938, 0.000000000000000000, -4.500000000000000888 ) ) ;
#3134=VERTEX_POINT ( 'NONE', #275 ) ;
#3141=TOROIDAL_SURFACE ( 'NONE', #3573, 3.100000000000000533, 0.1000000000000000056 ) ;
#3154=CIRCLE ( 'NONE', #3584, 0.1000000000000000472 ) ;
#3172=ORIENTED_EDGE ( 'NONE', *, *, #11194, .T. ) ;
#3180=ORIENTED_EDGE ( 'NONE', *, *, #8860, .F. ) ;
#3186=DIRECTION ( 'NONE',  ( 1.224646799147353207E-16, 0.000000000000000000, -1.000000000000000000 ) ) ;
#3193=ORIENTED_EDGE ( 'NONE', *, *, #13411, .F. ) ;
#3201=VERTEX_POINT ( 'NONE', #12331 ) ;
#3203=DIRECTION ( 'NONE',  ( 0.000000000000000000, 0.000000000000000000, -1.000000000000000000 ) ) ;
#3211=DIRECTION ( 'NONE',  ( 0.000000000000000000, 0.000000000000000000, 1.000000000000000000 ) ) ;
#3220=DIRECTION ( 'NONE',  ( 0.000000000000000000, 0.000000000000000000, 1.000000000000000000 ) ) ;
#3223=ORIENTED_EDGE ( 'NONE', *, *, #2279, .T. ) ;
#3238=VERTEX_POINT ( 'NONE', #2875 ) ;
#3247=DIRECTION ( 'NONE',  ( -0.000000000000000000, -1.000000000000000000, 0.000000000000000000 ) ) ;
#3249=CYLINDRICAL_SURFACE ( 'NONE', #8386, 3.000000000000000444 ) ;
#3264=VERTEX_POINT ( 'NONE', #7084 ) ;
#3268=CYLINDRICAL_SURFACE ( 'NONE', #1985, 1.500000000000000222 ) ;
#3277=VERTEX_POINT ( 'NONE', #10042 ) ;
#3291=CIRCLE ( 'NONE', #11000, 1.500000000000003997 ) ;
#3312=DIRECTION ( 'NONE',  ( 0.000000000000000000, 0.000000000000000000, 1.000000000000000000 ) ) ;
#3317=DIRECTION ( 'NONE',  ( 0.000000000000000000, 1.000000000000000000, -0.000000000000000000 ) ) ;
#3320=AXIS2_PLACEMENT_3D ( 'NONE', #7808, #13120, #1481 ) ;
#3321=EDGE_LOOP ( 'NONE', ( #1646, #2276, #12954, #8028 ) ) ;
#3341=EDGE_CURVE ( 'NONE', #7249, #2521, #6, .T. ) ;
#3344=CIRCLE ( 'NONE', #943, 3.000000000000000888 ) ;
#3346=DIRECTION ( 'NONE',  ( -1.000000000000000000, 0.000000000000000000, 0.000000000000000000 ) ) ;
#3348=DIRECTION ( 'NONE',  ( -0.6923076923076927347, 0.000000000000000000, 0.7216024245882196597 ) ) ;
#3349=DIRECTION ( 'NONE',  ( 0.000000000000000000, 1.000000000000000000, -0.000000000000000000 ) ) ;
#3352=ORIENTED_EDGE ( 'NONE', *, *, #8204, .F. ) ;
#3355=CARTESIAN_POINT ( 'NONE',  ( 0.000000000000000000, 2.900000000000000355, 0.000000000000000000 ) ) ;
#3366=ADVANCED_FACE ( 'NONE', ( #9559 ), #8554, .T. ) ;
#3374=ORIENTED_EDGE ( 'NONE', *, *, #11960, .T. ) ;
#3381=DIRECTION ( 'NONE',  ( 0.000000000000000000, 0.000000000000000000, 1.000000000000000000 ) ) ;
#3386=DIRECTION ( 'NONE',  ( 0.000000000000000000, 0.000000000000000000, 1.000000000000000000 ) ) ;
#3393=VECTOR ( 'NONE', #11992, 1000.000000000000000 ) ;
#3406=ORIENTED_EDGE ( 'NONE', *, *, #7448, .F. ) ;
#3412=ORIENTED_EDGE ( 'NONE', *, *, #13142, .T. ) ;
#3425=DIRECTION ( 'NONE',  ( 0.000000000000000000, 0.000000000000000000, 1.000000000000000000 ) ) ;
#3438=EDGE_CURVE ( 'NONE', #11405, #9031, #9673, .T. ) ;
#3461=ADVANCED_FACE ( 'NONE', ( #9417 ), #3268, .F. ) ;
#3467=CARTESIAN_POINT ( 'NONE',  ( 31.00000000000000000, 2.900000000000000355, 0.000000000000000000 ) ) ;
#3468=EDGE_CURVE ( 'NONE', #8871, #4931, #10590, .T. ) ;
#3480=FACE_BOUND ( 'NONE', #7468, .T. ) ;
#3481=DIRECTION ( 'NONE',  ( -0.6923076923076904032, 0.000000000000000000, 0.7216024245882218802 ) ) ;
#3490=DIRECTION ( 'NONE',  ( 0.000000000000000000, 1.000000000000000000, -0.000000000000000000 ) ) ;
#3495=CARTESIAN_POINT ( 'NONE',  ( 0.000000000000000000, 2.900000000000000355, 0.000000000000000000 ) ) ;
#3500=VERTEX_POINT ( 'NONE', #12159 ) ;
#3512=AXIS2_PLACEMENT_3D ( 'NONE', #13116, #5808, #6522 ) ;
#3516=FACE_OUTER_BOUND ( 'NONE', #7314, .T. ) ;
#3524=DIRECTION ( 'NONE',  ( 0.000000000000000000, 0.000000000000000000, 1.000000000000000000 ) ) ;
#3527=EDGE_CURVE ( 'NONE', #8040, #12695, #13421, .T. ) ;
#3533=FACE_OUTER_BOUND ( 'NONE', #13189, .T. ) ;
#3548=CIRCLE ( 'NONE', #11486, 0.1000000000000000472 ) ;
#3551=AXIS2_PLACEMENT_3D ( 'NONE', #976, #6006, #11438 ) ;
#3555=VERTEX_POINT ( 'NONE', #5880 ) ;
#3573=AXIS2_PLACEMENT_3D ( 'NONE', #1766, #6106, #8160 ) ;
#3578=ORIENTED_EDGE ( 'NONE', *, *, #8334, .F. ) ;
#3580=ORIENTED_EDGE ( 'NONE', *, *, #9398, .T. ) ;
#3584=AXIS2_PLACEMENT_3D ( 'NONE', #11256, #722, #5813 ) ;
#3609=CIRCLE ( 'NONE', #9567, 0.09999999999999982514 ) ;
#3631=CARTESIAN_POINT ( 'NONE',  ( 31.00000000000000000, -8.809142651444723526E-17, 1.600000000000004086 ) ) ;
#3637=DIRECTION ( 'NONE',  ( -0.000000000000000000, -1.000000000000000000, 0.000000000000000000 ) ) ;
#3643=EDGE_CURVE ( 'NONE', #2068, #1584, #7907, .T. ) ;
#3662=EDGE_CURVE ( 'NONE', #12096, #6347, #8082, .T. ) ;
#3663=CARTESIAN_POINT ( 'NONE',  ( 0.000000000000000000, 0.09999999999999982514, 1.399999999999999911 ) ) ;
#3690=CARTESIAN_POINT ( 'NONE',  ( 0.000000000000000000, 0.000000000000000000, 0.000000000000000000 ) ) ;
#3700=AXIS2_PLACEMENT_3D ( 'NONE', #8194, #12426, #7991 ) ;
#3701=CARTESIAN_POINT ( 'NONE',  ( 31.00000000000000000, 0.09999999999999982514, -1.600000000000004086 ) ) ;
#3705=EDGE_CURVE ( 'NONE', #10836, #937, #882, .T. ) ;
#3717=CARTESIAN_POINT ( 'NONE',  ( 31.00000000000000000, 2.900000000000000355, 0.000000000000000000 ) ) ;
#3736=DIRECTION ( 'NONE',  ( 0.000000000000000000, 1.000000000000000000, -0.000000000000000000 ) ) ;
#3738=DIRECTION ( 'NONE',  ( -0.000000000000000000, -1.000000000000000000, 0.000000000000000000 ) ) ;
#3740=FACE_OUTER_BOUND ( 'NONE', #9235, .T. ) ;
#3741=AXIS2_PLACEMENT_3D ( 'NONE', #11008, #3247, #3312 ) ;
#3756=DIRECTION ( 'NONE',  ( -0.000000000000000000, -1.000000000000000000, -0.000000000000000000 ) ) ;
#3785=ORIENTED_EDGE ( 'NONE', *, *, #3662, .T. ) ;
#3801=EDGE_CURVE ( 'NONE', #7249, #2378, #10116, .T. ) ;
#3802=ORIENTED_EDGE ( 'NONE', *, *, #10438, .T. ) ;
#3819=CARTESIAN_POINT ( 'NONE',  ( 0.000000000000000000, 0.09999999999999982514, 0.000000000000000000 ) ) ;
#3826=ORIENTED_EDGE ( 'NONE', *, *, #5654, .T. ) ;
#3839=ADVANCED_FACE ( 'NONE', ( #11798 ), #1394, .T. ) ;
#3850=CARTESIAN_POINT ( 'NONE',  ( 1.959434878635765477E-16, 0.09999999999999982514, -1.600000000000000311 ) ) ;
#3856=CIRCLE ( 'NONE', #345, 0.1000000000000000472 ) ;
#3869=DIRECTION ( 'NONE',  ( 0.000000000000000000, 0.000000000000000000, 1.000000000000000000 ) ) ;
#3871=ORIENTED_EDGE ( 'NONE', *, *, #1124, .F. ) ;
#3877=CARTESIAN_POINT ( 'NONE',  ( 31.00000000000000000, 3.000000000000000000, 0.000000000000000000 ) ) ;
#3882=CARTESIAN_POINT ( 'NONE',  ( 4.163799117101002038E-16, 2.900000000000000355, -3.400000000000001243 ) ) ;
#3910=CARTESIAN_POINT ( 'NONE',  ( 31.00000000000000000, -8.809142651444723526E-17, -1.600000000000004086 ) ) ;
#3921=ADVANCED_BREP_SHAPE_REPRESENTATION ( '', ( #13227, #10007 ), #1673 ) ;
#3928=FACE_BOUND ( 'NONE', #9012, .T. ) ;
#3942=DIRECTION ( 'NONE',  ( 0.000000000000000000, 0.000000000000000000, 1.000000000000000000 ) ) ;
#3943=CARTESIAN_POINT ( 'NONE',  ( 31.00000000000000000, 2.900000000000000355, 0.000000000000000000 ) ) ;
#3965=CARTESIAN_POINT ( 'NONE',  ( 31.00000000000000000, 2.900000000000000355, -3.499999999999999556 ) ) ;
#3969=AXIS2_PLACEMENT_3D ( 'NONE', #8511, #5219, #5282 ) ;
#3990=VERTEX_POINT ( 'NONE', #12494 ) ;
#3998=ORIENTED_EDGE ( 'NONE', *, *, #5571, .F. ) ;
#4013=AXIS2_PLACEMENT_3D ( 'NONE', #8605, #10558, #1119 ) ;
#4016=DIRECTION ( 'NONE',  ( 0.000000000000000000, 0.000000000000000000, 1.000000000000000000 ) ) ;
#4017=DIRECTION ( 'NONE',  ( 0.000000000000000000, 1.000000000000000000, -0.000000000000000000 ) ) ;
#4035=CIRCLE ( 'NONE', #8429, 1.500000000000003997 ) ;
#4039=DIRECTION ( 'NONE',  ( 0.000000000000000000, 0.000000000000000000, 1.000000000000000000 ) ) ;
#4066=AXIS2_PLACEMENT_3D ( 'NONE', #1469, #3317, #4423 ) ;
#4072=EDGE_CURVE ( 'NONE', #13228, #10250, #1116, .T. ) ;
#4094=DIRECTION ( 'NONE',  ( 0.000000000000000000, 0.000000000000000000, -1.000000000000000000 ) ) ;
#4122=ORIENTED_EDGE ( 'NONE', *, *, #10783, .F. ) ;
#4125=DIRECTION ( 'NONE',  ( 0.000000000000000000, 1.000000000000000000, -0.000000000000000000 ) ) ;
#4142=ORIENTED_EDGE ( 'NONE', *, *, #1447, .T. ) ;
#4149=DIRECTION ( 'NONE',  ( 0.7216024245882196597, 0.000000000000000000, -0.6923076923076926237 ) ) ;
#4157=ORIENTED_EDGE ( 'NONE', *, *, #12051, .T. ) ;
#4161=ORIENTED_EDGE ( 'NONE', *, *, #12581, .F. ) ;
#4167=CIRCLE ( 'NONE', #1093, 3.100000000000000533 ) ;
#4170=DIRECTION ( 'NONE',  ( 0.000000000000000000, 0.000000000000000000, 1.000000000000000000 ) ) ;
#4175=CIRCLE ( 'NONE', #2199, 0.1000000000000001166 ) ;
#4179=LINE ( 'NONE', #11690, #8803 ) ;
#4180=FACE_OUTER_BOUND ( 'NONE', #6889, .T. ) ;
#4184=AXIS2_PLACEMENT_3D ( 'NONE', #11330, #4017, #3942 ) ;
#4195=AXIS2_PLACEMENT_3D ( 'NONE', #13012, #7641, #9899 ) ;
#4207=DIRECTION ( 'NONE',  ( 0.000000000000000000, 0.000000000000000000, 1.000000000000000000 ) ) ;
#4221=ORIENTED_EDGE ( 'NONE', *, *, #5062, .F. ) ;
#4226=CIRCLE ( 'NONE', #11933, 0.1000000000000000472 ) ;
#4227=ADVANCED_FACE ( 'NONE', ( #6602 ), #13217, .T. ) ;
#4242=DIRECTION ( 'NONE',  ( 0.000000000000000000, 0.000000000000000000, 1.000000000000000000 ) ) ;
#4245=TOROIDAL_SURFACE ( 'NONE', #12177, 3.400000000000001243, 0.1000000000000000056 ) ;
#4250=CARTESIAN_POINT ( 'NONE',  ( 26.30958424017656938, 0.09999999999999982514, 1.500000000000000000 ) ) ;
#4257=VECTOR ( 'NONE', #1880, 1000.000000000000000 ) ;
#4266=SURFACE_STYLE_FILL_AREA ( #7304 ) ;
#4267=AXIS2_PLACEMENT_3D ( 'NONE', #1860, #3081, #10183 ) ;
#4291=CARTESIAN_POINT ( 'NONE',  ( 31.00000000000000000, 3.000000000000000000, 0.000000000000000000 ) ) ;
#4293=DIRECTION ( 'NONE',  ( -0.000000000000000000, -1.000000000000000000, -0.000000000000000000 ) ) ;
#4306=EDGE_CURVE ( 'NONE', #10281, #5856, #10139, .T. ) ;
#4322=DIRECTION ( 'NONE',  ( 0.000000000000000000, 0.000000000000000000, 1.000000000000000000 ) ) ;
#4326=DIRECTION ( 'NONE',  ( 0.7216024245882196597, 0.000000000000000000, 0.6923076923076926237 ) ) ;
#4333=ORIENTED_EDGE ( 'NONE', *, *, #10954, .F. ) ;
#4334=DIRECTION ( 'NONE',  ( 0.000000000000000000, 0.000000000000000000, 1.000000000000000000 ) ) ;
#4371=DIRECTION ( 'NONE',  ( 0.000000000000000000, 1.000000000000000000, -0.000000000000000000 ) ) ;
#4382=CARTESIAN_POINT ( 'NONE',  ( 0.000000000000000000, 3.000000000000000000, 0.000000000000000000 ) ) ;
#4384=CARTESIAN_POINT ( 'NONE',  ( 4.690415759823430619, 2.900000000000000355, -1.399999999999999911 ) ) ;
#4391=EDGE_LOOP ( 'NONE', ( #6804, #11958, #5166, #1498 ) ) ;
#4394=AXIS2_PLACEMENT_3D ( 'NONE', #2170, #11613, #6239 ) ;
#4409=ORIENTED_EDGE ( 'NONE', *, *, #10627, .F. ) ;
#4412=EDGE_LOOP ( 'NONE', ( #3406, #5009, #2985, #11712 ) ) ;
#4416=AXIS2_PLACEMENT_3D ( 'NONE', #1578, #4749, #2670 ) ;
#4423=DIRECTION ( 'NONE',  ( 0.000000000000000000, 0.000000000000000000, 1.000000000000000000 ) ) ;
#4457=VERTEX_POINT ( 'NONE', #1721 ) ;
#4458=EDGE_LOOP ( 'NONE', ( #7842, #25, #4864, #13544 ) ) ;
#4459=AXIS2_PLACEMENT_3D ( 'NONE', #12423, #10397, #898 ) ;
#4464=ORIENTED_EDGE ( 'NONE', *, *, #8297, .F. ) ;
#4465=DIRECTION ( 'NONE',  ( -1.000000000000000000, 0.000000000000000000, 0.000000000000000000 ) ) ;
#4490=DIRECTION ( 'NONE',  ( -1.000000000000000000, 0.000000000000000000, 0.000000000000000000 ) ) ;
#4491=CARTESIAN_POINT ( 'NONE',  ( 26.30958424017656938, 2.900000000000000355, 4.500000000000000888 ) ) ;
#4507=AXIS2_PLACEMENT_3D ( 'NONE', #12290, #11240, #9099 ) ;
#4511=CARTESIAN_POINT ( 'NONE',  ( 28.54655175640005282, 0.000000000000000000, 2.353846153846155254 ) ) ;
#4513=CARTESIAN_POINT ( 'NONE',  ( 4.690415759823430619, 0.1000000000000000056, 1.399999999999999911 ) ) ;
#4517=TOROIDAL_SURFACE ( 'NONE', #1218, 3.399999999999999911, 0.1000000000000000056 ) ;
#4519=DIRECTION ( 'NONE',  ( 0.000000000000000000, 0.000000000000000000, -1.000000000000000000 ) ) ;
#4524=CARTESIAN_POINT ( 'NONE',  ( 31.00000000000000000, 0.09999999999999982514, 0.000000000000000000 ) ) ;
#4546=ORIENTED_EDGE ( 'NONE', *, *, #2379, .F. ) ;
#4550=EDGE_CURVE ( 'NONE', #2353, #4598, #5078, .T. ) ;
#4579=ORIENTED_EDGE ( 'NONE', *, *, #7221, .F. ) ;
#4586=DIRECTION ( 'NONE',  ( 0.000000000000000000, 0.000000000000000000, 1.000000000000000000 ) ) ;
#4587=CARTESIAN_POINT ( 'NONE',  ( 2.453448243599949397, 3.000000000000000000, 2.353846153846154365 ) ) ;
#4589=FACE_OUTER_BOUND ( 'NONE', #7187, .T. ) ;
#4596=ORIENTED_EDGE ( 'NONE', *, *, #11489, .T. ) ;
#4598=VERTEX_POINT ( 'NONE', #4250 ) ;
#4612=ORIENTED_EDGE ( 'NONE', *, *, #3113, .T. ) ;
#4623=CYLINDRICAL_SURFACE ( 'NONE', #8893, 3.000000000000000888 ) ;
#4626=EDGE_CURVE ( 'NONE', #2353, #2068, #4179, .T. ) ;
#4645=VERTEX_POINT ( 'NONE', #2525 ) ;
#4651=DIRECTION ( 'NONE',  ( -0.000000000000000000, -1.000000000000000000, 0.000000000000000000 ) ) ;
#4655=DIRECTION ( 'NONE',  ( 0.000000000000000000, 0.000000000000000000, 1.000000000000000000 ) ) ;
#4678=EDGE_CURVE ( 'NONE', #7143, #11405, #13444, .T. ) ;
#4685=EDGE_LOOP ( 'NONE', ( #1340, #1677, #9802, #10763 ) ) ;
#4691=AXIS2_PLACEMENT_3D ( 'NONE', #450, #4651, #12035 ) ;
#4699=DIRECTION ( 'NONE',  ( 1.000000000000000000, -0.000000000000000000, 0.000000000000000000 ) ) ;
#4714=DIRECTION ( 'NONE',  ( 0.000000000000000000, 0.000000000000000000, 1.000000000000000000 ) ) ;
#4724=ADVANCED_FACE ( 'NONE', ( #4589, #3480, #9683 ), #332, .F. ) ;
#4738=DIRECTION ( 'NONE',  ( 1.000000000000000000, 0.000000000000000000, 1.224646799147353207E-16 ) ) ;
#4749=DIRECTION ( 'NONE',  ( -0.000000000000000000, -1.000000000000000000, 0.000000000000000000 ) ) ;
#4757=ORIENTED_EDGE ( 'NONE', *, *, #2446, .T. ) ;
#4774=ORIENTED_EDGE ( 'NONE', *, *, #1059, .F. ) ;
#4799=EDGE_CURVE ( 'NONE', #8041, #7779, #7503, .T. ) ;
#4805=ORIENTED_EDGE ( 'NONE', *, *, #9624, .F. ) ;
#4819=DIRECTION ( 'NONE',  ( -0.000000000000000000, -1.000000000000000000, 0.000000000000000000 ) ) ;
#4830=DIRECTION ( 'NONE',  ( -0.000000000000000000, -1.000000000000000000, 0.000000000000000000 ) ) ;
#4833=ORIENTED_EDGE ( 'NONE', *, *, #13209, .F. ) ;
#4837=TOROIDAL_SURFACE ( 'NONE', #5487, 3.100000000000000977, 0.1000000000000000056 ) ;
#4847=ADVANCED_FACE ( 'NONE', ( #12468 ), #4837, .T. ) ;
#4854=ORIENTED_EDGE ( 'NONE', *, *, #10783, .T. ) ;
#4864=ORIENTED_EDGE ( 'NONE', *, *, #1543, .T. ) ;
#4865=AXIS2_PLACEMENT_3D ( 'NONE', #4513, #1273, #11817 ) ;
#4890=EDGE_LOOP ( 'NONE', ( #4546, #4221, #8890, #7287 ) ) ;
#4906=ORIENTED_EDGE ( 'NONE', *, *, #2054, .T. ) ;
#4922=DIRECTION ( 'NONE',  ( 1.224646799147353454E-16, 0.000000000000000000, -1.000000000000000000 ) ) ;
#4924=AXIS2_PLACEMENT_3D ( 'NONE', #3943, #3736, #5882 ) ;
#4927=VERTEX_POINT ( 'NONE', #12587 ) ;
#4929=EDGE_CURVE ( 'NONE', #3134, #12940, #6596, .T. ) ;
#4931=VERTEX_POINT ( 'NONE', #7411 ) ;
#4932=DIRECTION ( 'NONE',  ( 0.000000000000000000, 1.000000000000000000, -0.000000000000000000 ) ) ;
#4934=DIRECTION ( 'NONE',  ( -0.000000000000000000, -1.000000000000000000, -0.000000000000000000 ) ) ;
#4937=DIRECTION ( 'NONE',  ( 1.000000000000000000, -0.000000000000000000, 0.000000000000000000 ) ) ;
#4940=( GEOMETRIC_REPRESENTATION_CONTEXT ( 3 ) GLOBAL_UNCERTAINTY_ASSIGNED_CONTEXT ( ( #6809 ) ) GLOBAL_UNIT_ASSIGNED_CONTEXT ( ( #10648, #5401, #123 ) ) REPRESENTATION_CONTEXT ( 'NONE', 'WORKASPACE' ) );
#4942=CIRCLE ( 'NONE', #10662, 0.1000000000000001166 ) ;
#4945=TOROIDAL_SURFACE ( 'NONE', #13308, 3.100000000000000977, 0.1000000000000000056 ) ;
#4961=ADVANCED_FACE ( 'NONE', ( #8361 ), #12760, .T. ) ;
#4968=CARTESIAN_POINT ( 'NONE',  ( 0.000000000000000000, 2.900000000000000355, 0.000000000000000000 ) ) ;
#4988=CARTESIAN_POINT ( 'NONE',  ( 31.00000000000000000, 0.09999999999999982514, 0.000000000000000000 ) ) ;
#5001=CARTESIAN_POINT ( 'NONE',  ( 28.54655175640005282, 2.900000000000000355, 2.353846153846155254 ) ) ;
#5009=ORIENTED_EDGE ( 'NONE', *, *, #12723, .F. ) ;
#5035=ORIENTED_EDGE ( 'NONE', *, *, #10540, .F. ) ;
#5055=EDGE_LOOP ( 'NONE', ( #8581, #9745, #7912, #12369 ) ) ;
#5062=EDGE_CURVE ( 'NONE', #2354, #594, #7269, .T. ) ;
#5064=DIRECTION ( 'NONE',  ( 0.000000000000000000, 1.000000000000000000, -0.000000000000000000 ) ) ;
#5073=ORIENTED_EDGE ( 'NONE', *, *, #1932, .F. ) ;
#5077=CIRCLE ( 'NONE', #10792, 0.1000000000000000472 ) ;
#5078=CIRCLE ( 'NONE', #9030, 0.1000000000000000472 ) ;
#5093=DIRECTION ( 'NONE',  ( 0.000000000000000000, 0.000000000000000000, 1.000000000000000000 ) ) ;
#5098=DIRECTION ( 'NONE',  ( -0.000000000000000000, -1.000000000000000000, 0.000000000000000000 ) ) ;
#5108=ORIENTED_EDGE ( 'NONE', *, *, #6160, .F. ) ;
#5114=LINE ( 'NONE', #11180, #1432 ) ;
#5139=CIRCLE ( 'NONE', #1843, 1.600000000000000311 ) ;
#5140=AXIS2_PLACEMENT_3D ( 'NONE', #11203, #9348, #6049 ) ;
#5154=DIRECTION ( 'NONE',  ( 0.000000000000000000, 1.000000000000000000, -0.000000000000000000 ) ) ;
#5164=ORIENTED_EDGE ( 'NONE', *, *, #1316, .T. ) ;
#5166=ORIENTED_EDGE ( 'NONE', *, *, #1030, .F. ) ;
#5169=AXIS2_PLACEMENT_3D ( 'NONE', #1010, #11673, #9543 ) ;
#5217=DIRECTION ( 'NONE',  ( 1.000000000000000000, -0.000000000000000000, 0.000000000000000000 ) ) ;
#5219=DIRECTION ( 'NONE',  ( 0.000000000000000000, 1.000000000000000000, -0.000000000000000000 ) ) ;
#5228=ORIENTED_EDGE ( 'NONE', *, *, #5265, .F. ) ;
#5230=( LENGTH_UNIT ( ) NAMED_UNIT ( * ) SI_UNIT ( .MILLI., .METRE. ) );
#5231=DIRECTION ( 'NONE',  ( 0.000000000000000000, 0.000000000000000000, 1.000000000000000000 ) ) ;
#5246=DIRECTION ( 'NONE',  ( -0.000000000000000000, -1.000000000000000000, -0.000000000000000000 ) ) ;
#5252=DIRECTION ( 'NONE',  ( 0.6923076923076925127, 0.000000000000000000, 0.7216024245882197707 ) ) ;
#5261=EDGE_LOOP ( 'NONE', ( #5674, #4612, #10599, #3412 ) ) ;
#5265=EDGE_CURVE ( 'NONE', #7779, #1278, #3085, .T. ) ;
#5282=DIRECTION ( 'NONE',  ( 0.000000000000000000, 0.000000000000000000, 1.000000000000000000 ) ) ;
#5327=TOROIDAL_SURFACE ( 'NONE', #5764, 3.400000000000001243, 0.1000000000000000056 ) ;
#5340=CIRCLE ( 'NONE', #7983, 3.100000000000000977 ) ;
#5364=FACE_OUTER_BOUND ( 'NONE', #10675, .T. ) ;
#5378=STYLED_ITEM('',(#13635),#13227);
#5387=FACE_OUTER_BOUND ( 'NONE', #13243, .T. ) ;
#5388=AXIS2_PLACEMENT_3D ( 'NONE', #3701, #2813, #7901 ) ;
#5401=( NAMED_UNIT ( * ) PLANE_ANGLE_UNIT ( ) SI_UNIT ( $, .RADIAN. ) );
#5411=EDGE_CURVE ( 'NONE', #7143, #5856, #12160, .T. ) ;
#5416=CARTESIAN_POINT ( 'NONE',  ( 0.000000000000000000, 2.900000000000000355, 0.000000000000000000 ) ) ;
#5421=DIRECTION ( 'NONE',  ( 0.000000000000000000, 0.000000000000000000, 1.000000000000000000 ) ) ;
#5435=FACE_OUTER_BOUND ( 'NONE', #7622, .T. ) ;
#5451=FACE_OUTER_BOUND ( 'NONE', #8722, .T. ) ;
#5455=ORIENTED_EDGE ( 'NONE', *, *, #210, .T. ) ;
#5464=DIRECTION ( 'NONE',  ( 0.000000000000000000, 0.000000000000000000, 1.000000000000000000 ) ) ;
#5473=DIRECTION ( 'NONE',  ( 0.000000000000000000, 1.000000000000000000, -0.000000000000000000 ) ) ;
#5476=EDGE_CURVE ( 'NONE', #10281, #8802, #10344, .T. ) ;
#5482=ORIENTED_EDGE ( 'NONE', *, *, #5062, .T. ) ;
#5487=AXIS2_PLACEMENT_3D ( 'NONE', #13275, #8032, #7073 ) ;
#5490=VERTEX_POINT ( 'NONE', #5735 ) ;
#5496=DIRECTION ( 'NONE',  ( -0.000000000000000000, -1.000000000000000000, 0.000000000000000000 ) ) ;
#5508=AXIS2_PLACEMENT_3D ( 'NONE', #8845, #3481, #9883 ) ;
#5554=DIRECTION ( 'NONE',  ( 0.000000000000000000, 0.000000000000000000, 1.000000000000000000 ) ) ;
#5571=EDGE_CURVE ( 'NONE', #9479, #3134, #6167, .T. ) ;
#5590=DIRECTION ( 'NONE',  ( 0.000000000000000000, 0.000000000000000000, -1.000000000000000000 ) ) ;
#5592=EDGE_CURVE ( 'NONE', #2583, #12211, #4175, .T. ) ;
#5631=DIRECTION ( 'NONE',  ( 0.000000000000000000, 0.000000000000000000, 1.000000000000000000 ) ) ;
#5636=EDGE_CURVE ( 'NONE', #1237, #10281, #1551, .T. ) ;
#5654=EDGE_CURVE ( 'NONE', #12265, #4927, #3291, .T. ) ;
#5665=EDGE_CURVE ( 'NONE', #9614, #12211, #9680, .T. ) ;
#5674=ORIENTED_EDGE ( 'NONE', *, *, #7176, .F. ) ;
#5678=ORIENTED_EDGE ( 'NONE', *, *, #181, .T. ) ;
#5682=FACE_OUTER_BOUND ( 'NONE', #11111, .T. ) ;
#5685=CARTESIAN_POINT ( 'NONE',  ( 31.00000000000000000, 3.000000000000000000, 0.000000000000000000 ) ) ;
#5695=AXIS2_PLACEMENT_3D ( 'NONE', #13144, #4465, #10939 ) ;
#5712=DIRECTION ( 'NONE',  ( 1.000000000000000000, 0.000000000000000000, 0.000000000000000000 ) ) ;
#5720=CARTESIAN_POINT ( 'NONE',  ( 0.000000000000000000, 0.09999999999999982514, -3.500000000000000888 ) ) ;
#5725=CIRCLE ( 'NONE', #3969, 3.000000000000000444 ) ;
#5735=CARTESIAN_POINT ( 'NONE',  ( 0.000000000000000000, -8.809142651444723526E-17, 1.600000000000000311 ) ) ;
#5743=ORIENTED_EDGE ( 'NONE', *, *, #1447, .F. ) ;
#5746=AXIS2_PLACEMENT_3D ( 'NONE', #3663, #2776, #2704 ) ;
#5757=CARTESIAN_POINT ( 'NONE',  ( 0.000000000000000000, 0.000000000000000000, 0.000000000000000000 ) ) ;
#5764=AXIS2_PLACEMENT_3D ( 'NONE', #4968, #698, #8066 ) ;
#5767=VECTOR ( 'NONE', #12373, 1000.000000000000000 ) ;
#5781=EDGE_LOOP ( 'NONE', ( #10707, #9191, #10325, #2192 ) ) ;
#5795=DIRECTION ( 'NONE',  ( 0.000000000000000000, 1.000000000000000000, -0.000000000000000000 ) ) ;
#5808=DIRECTION ( 'NONE',  ( -0.000000000000000000, -1.000000000000000000, 0.000000000000000000 ) ) ;
#5813=DIRECTION ( 'NONE',  ( 0.000000000000000000, 0.000000000000000000, -1.000000000000000000 ) ) ;
#5815=EDGE_CURVE ( 'NONE', #4598, #13228, #12123, .T. ) ;
#5824=AXIS2_PLACEMENT_3D ( 'NONE', #12075, #2767, #13106 ) ;
#5828=EDGE_CURVE ( 'NONE', #9614, #8871, #5077, .T. ) ;
#5852=ORIENTED_EDGE ( 'NONE', *, *, #10574, .F. ) ;
#5853=ORIENTED_EDGE ( 'NONE', *, *, #1229, .T. ) ;
#5856=VERTEX_POINT ( 'NONE', #11082 ) ;
#5871=DIRECTION ( 'NONE',  ( 0.000000000000000000, 0.000000000000000000, 1.000000000000000000 ) ) ;
#5880=CARTESIAN_POINT ( 'NONE',  ( 1.959434878635765477E-16, -8.809142651444723526E-17, -1.600000000000000311 ) ) ;
#5882=DIRECTION ( 'NONE',  ( 0.000000000000000000, 0.000000000000000000, 1.000000000000000000 ) ) ;
#5905=EDGE_CURVE ( 'NONE', #7779, #4457, #5725, .T. ) ;
#5910=CARTESIAN_POINT ( 'NONE',  ( 4.690415759823430619, 0.1000000000000000056, -1.399999999999999911 ) ) ;
#5915=DIRECTION ( 'NONE',  ( -0.000000000000000000, -1.000000000000000000, -0.000000000000000000 ) ) ;
#5927=DIRECTION ( 'NONE',  ( -1.000000000000000000, 0.000000000000000000, 0.000000000000000000 ) ) ;
#5952=CIRCLE ( 'NONE', #26, 0.1000000000000000472 ) ;
#5956=EDGE_LOOP ( 'NONE', ( #12117, #9860, #4161, #10571 ) ) ;
#5978=ADVANCED_FACE ( 'NONE', ( #4180 ), #10137, .T. ) ;
#5991=ORIENTED_EDGE ( 'NONE', *, *, #1049, .F. ) ;
#5993=TOROIDAL_SURFACE ( 'NONE', #1821, 3.400000000000001243, 0.1000000000000000056 ) ;
#6004=AXIS2_PLACEMENT_3D ( 'NONE', #10478, #11375, #5231 ) ;
#6005=AXIS2_PLACEMENT_3D ( 'NONE', #13261, #13123, #7947 ) ;
#6006=DIRECTION ( 'NONE',  ( -0.000000000000000000, -1.000000000000000000, 0.000000000000000000 ) ) ;
#6011=ORIENTED_EDGE ( 'NONE', *, *, #3006, .F. ) ;
#6015=CIRCLE ( 'NONE', #4459, 0.1000000000000001166 ) ;
#6017=AXIS2_PLACEMENT_3D ( 'NONE', #11380, #1945, #6138 ) ;
#6028=AXIS2_PLACEMENT_3D ( 'NONE', #1758, #517, #7138 ) ;
#6029=DIRECTION ( 'NONE',  ( 1.000000000000000000, 0.000000000000000000, 1.224646799147353207E-16 ) ) ;
#6030=CYLINDRICAL_SURFACE ( 'NONE', #6005, 1.500000000000000222 ) ;
#6041=EDGE_CURVE ( 'NONE', #12613, #11405, #6829, .T. ) ;
#6045=DIRECTION ( 'NONE',  ( -0.000000000000000000, -1.000000000000000000, 0.000000000000000000 ) ) ;
#6047=CARTESIAN_POINT ( 'NONE',  ( 31.00000000000000000, 2.900000000000000355, 0.000000000000000000 ) ) ;
#6049=DIRECTION ( 'NONE',  ( 0.000000000000000000, 0.000000000000000000, 1.000000000000000000 ) ) ;
#6052=DIRECTION ( 'NONE',  ( 0.000000000000000000, 1.000000000000000000, -0.000000000000000000 ) ) ;
#6053=DIRECTION ( 'NONE',  ( -0.000000000000000000, -1.000000000000000000, -0.000000000000000000 ) ) ;
#6054=VERTEX_POINT ( 'NONE', #13067 ) ;
#6069=VERTEX_POINT ( 'NONE', #10787 ) ;
#6091=CARTESIAN_POINT ( 'NONE',  ( 31.00000000000000000, 0.000000000000000000, 0.000000000000000000 ) ) ;
#6106=DIRECTION ( 'NONE',  ( 0.000000000000000000, 1.000000000000000000, -0.000000000000000000 ) ) ;
#6111=ORIENTED_EDGE ( 'NONE', *, *, #1932, .T. ) ;
#6138=DIRECTION ( 'NONE',  ( 0.000000000000000000, 0.000000000000000000, -1.000000000000000000 ) ) ;
#6160=EDGE_CURVE ( 'NONE', #4457, #6631, #5952, .T. ) ;
#6166=DIRECTION ( 'NONE',  ( 0.000000000000000000, 0.000000000000000000, -1.000000000000000000 ) ) ;
#6167=CIRCLE ( 'NONE', #4184, 3.400000000000001243 ) ;
#6207=TOROIDAL_SURFACE ( 'NONE', #9720, 3.100000000000000533, 0.1000000000000000056 ) ;
#6213=DIRECTION ( 'NONE',  ( 0.000000000000000000, 1.000000000000000000, -0.000000000000000000 ) ) ;
#6220=DIRECTION ( 'NONE',  ( 0.000000000000000000, 0.000000000000000000, 1.000000000000000000 ) ) ;
#6239=DIRECTION ( 'NONE',  ( 0.000000000000000000, 0.000000000000000000, 1.000000000000000000 ) ) ;
#6256=DIRECTION ( 'NONE',  ( 0.000000000000000000, 1.000000000000000000, -0.000000000000000000 ) ) ;
#6261=DIRECTION ( 'NONE',  ( -0.000000000000000000, -1.000000000000000000, -0.000000000000000000 ) ) ;
#6266=CARTESIAN_POINT ( 'NONE',  ( 0.000000000000000000, 0.000000000000000000, 0.000000000000000000 ) ) ;
#6293=ORIENTED_EDGE ( 'NONE', *, *, #3438, .F. ) ;
#6308=FACE_OUTER_BOUND ( 'NONE', #4412, .T. ) ;
#6319=FACE_OUTER_BOUND ( 'NONE', #9674, .T. ) ;
#6326=LINE ( 'NONE', #11371, #7981 ) ;
#6331=( NAMED_UNIT ( * ) PLANE_ANGLE_UNIT ( ) SI_UNIT ( $, .RADIAN. ) );
#6347=VERTEX_POINT ( 'NONE', #9410 ) ;
#6382=FACE_OUTER_BOUND ( 'NONE', #13007, .T. ) ;
#6401=CARTESIAN_POINT ( 'NONE',  ( 31.00000000000000000, 3.000000000000000000, 0.000000000000000000 ) ) ;
#6461=AXIS2_PLACEMENT_3D ( 'NONE', #13347, #4932, #7274 ) ;
#6462=CARTESIAN_POINT ( 'NONE',  ( 28.54655175640005282, 0.000000000000000000, -2.353846153846155254 ) ) ;
#6465=ORIENTED_EDGE ( 'NONE', *, *, #6570, .T. ) ;
#6472=TOROIDAL_SURFACE ( 'NONE', #541, 1.600000000000000311, 0.1000000000000000056 ) ;
#6482=EDGE_CURVE ( 'NONE', #2068, #11685, #10366, .T. ) ;
#6488=DIRECTION ( 'NONE',  ( 0.000000000000000000, 0.000000000000000000, 1.000000000000000000 ) ) ;
#6498=VERTEX_POINT ( 'NONE', #382 ) ;
#6500=ADVANCED_FACE ( 'NONE', ( #8702 ), #11021, .T. ) ;
#6511=CARTESIAN_POINT ( 'NONE',  ( 26.30958424017656938, 0.09999999999999982514, 4.500000000000000888 ) ) ;
#6522=DIRECTION ( 'NONE',  ( 0.000000000000000000, 0.000000000000000000, 1.000000000000000000 ) ) ;
#6534=DIRECTION ( 'NONE',  ( 0.000000000000000000, 1.000000000000000000, -0.000000000000000000 ) ) ;
#6546=ORIENTED_EDGE ( 'NONE', *, *, #11908, .F. ) ;
#6550=ORIENTED_EDGE ( 'NONE', *, *, #4799, .F. ) ;
#6556=FACE_OUTER_BOUND ( 'NONE', #10155, .T. ) ;
#6566=ORIENTED_EDGE ( 'NONE', *, *, #10540, .T. ) ;
#6569=ADVANCED_FACE ( 'NONE', ( #3533 ), #6843, .T. ) ;
#6570=EDGE_CURVE ( 'NONE', #6347, #11521, #12585, .T. ) ;
#6586=CIRCLE ( 'NONE', #5695, 0.09999999999999982514 ) ;
#6587=CARTESIAN_POINT ( 'NONE',  ( 2.453448243599948952, 0.1000000000000000056, 2.353846153846153921 ) ) ;
#6592=ORIENTED_EDGE ( 'NONE', *, *, #181, .F. ) ;
#6595=CARTESIAN_POINT ( 'NONE',  ( 0.000000000000000000, 3.000000000000000000, -1.500000000000000222 ) ) ;
#6596=CIRCLE ( 'NONE', #4394, 3.400000000000001243 ) ;
#6598=ORIENTED_EDGE ( 'NONE', *, *, #5828, .F. ) ;
#6602=FACE_OUTER_BOUND ( 'NONE', #5956, .T. ) ;
#6618=ORIENTED_EDGE ( 'NONE', *, *, #11873, .F. ) ;
#6631=VERTEX_POINT ( 'NONE', #13121 ) ;
#6641=DIRECTION ( 'NONE',  ( -0.000000000000000000, -1.000000000000000000, 0.000000000000000000 ) ) ;
#6642=ORIENTED_EDGE ( 'NONE', *, *, #9370, .F. ) ;
#6643=AXIS2_PLACEMENT_3D ( 'NONE', #2177, #10854, #4242 ) ;
#6646=DIRECTION ( 'NONE',  ( 1.000000000000000000, 0.000000000000000000, 1.224646799147353207E-16 ) ) ;
#6654=CYLINDRICAL_SURFACE ( 'NONE', #10175, 0.1000000000000000472 ) ;
#6656=AXIS2_PLACEMENT_3D ( 'NONE', #3037, #2978, #10415 ) ;
#6667=AXIS2_PLACEMENT_3D ( 'NONE', #11430, #968, #5093 ) ;
#6670=TOROIDAL_SURFACE ( 'NONE', #13041, 1.600000000000004086, 0.1000000000000000056 ) ;
#6672=ORIENTED_EDGE ( 'NONE', *, *, #8385, .T. ) ;
#6680=TOROIDAL_SURFACE ( 'NONE', #8857, 3.399999999999999911, 0.1000000000000000056 ) ;
#6694=DIRECTION ( 'NONE',  ( 0.000000000000000000, 0.000000000000000000, 1.000000000000000000 ) ) ;
#6701=VECTOR ( 'NONE', #12122, 1000.000000000000000 ) ;
#6704=VERTEX_POINT ( 'NONE', #12570 ) ;
#6713=CARTESIAN_POINT ( 'NONE',  ( 0.000000000000000000, 2.900000000000000355, 0.000000000000000000 ) ) ;
#6716=TOROIDAL_SURFACE ( 'NONE', #8472, 1.600000000000000311, 0.1000000000000000056 ) ;
#6722=FACE_OUTER_BOUND ( 'NONE', #1402, .T. ) ;
#6733=CARTESIAN_POINT ( 'NONE',  ( 31.00000000000000000, 0.000000000000000000, 0.000000000000000000 ) ) ;
#6754=CARTESIAN_POINT ( 'NONE',  ( 0.000000000000000000, 0.000000000000000000, 0.000000000000000000 ) ) ;
#6775=DIRECTION ( 'NONE',  ( -0.000000000000000000, -1.000000000000000000, 0.000000000000000000 ) ) ;
#6778=DIRECTION ( 'NONE',  ( 0.000000000000000000, 1.000000000000000000, -0.000000000000000000 ) ) ;
#6780=ORIENTED_EDGE ( 'NONE', *, *, #6160, .T. ) ;
#6785=DIRECTION ( 'NONE',  ( 0.000000000000000000, 0.000000000000000000, 1.000000000000000000 ) ) ;
#6792=ORIENTED_EDGE ( 'NONE', *, *, #12051, .F. ) ;
#6804=ORIENTED_EDGE ( 'NONE', *, *, #11329, .F. ) ;
#6809=UNCERTAINTY_MEASURE_WITH_UNIT (LENGTH_MEASURE( 1.000000000000000082E-05 ), #10648, 'distance_accuracy_value', 'NONE');
#6819=CARTESIAN_POINT ( 'NONE',  ( 31.00000000000000000, 0.09999999999999982514, 0.000000000000000000 ) ) ;
#6829=CIRCLE ( 'NONE', #5508, 0.09999999999999982514 ) ;
#6834=ADVANCED_FACE ( 'NONE', ( #5451 ), #3249, .F. ) ;
#6843=TOROIDAL_SURFACE ( 'NONE', #7715, 3.400000000000001243, 0.1000000000000000056 ) ;
#6844=DIRECTION ( 'NONE',  ( 0.7216024245882196597, 0.000000000000000000, -0.6923076923076926237 ) ) ;
#6849=ORIENTED_EDGE ( 'NONE', *, *, #8272, .F. ) ;
#6857=CARTESIAN_POINT ( 'NONE',  ( 26.30958424017656938, 2.900000000000000355, -4.500000000000000888 ) ) ;
#6876=DIRECTION ( 'NONE',  ( 0.000000000000000000, 0.000000000000000000, 1.000000000000000000 ) ) ;
#6884=ORIENTED_EDGE ( 'NONE', *, *, #197, .F. ) ;
#6889=EDGE_LOOP ( 'NONE', ( #4833, #12456, #10038, #4122 ) ) ;
#6906=CIRCLE ( 'NONE', #12847, 3.399999999999999911 ) ;
#6916=CIRCLE ( 'NONE', #1423, 1.500000000000000222 ) ;
#6927=CIRCLE ( 'NONE', #7798, 3.399999999999999911 ) ;
#6941=CARTESIAN_POINT ( 'NONE',  ( 4.690415759823430619, 0.000000000000000000, -1.399999999999999911 ) ) ;
#6943=EDGE_CURVE ( 'NONE', #4645, #4598, #7527, .T. ) ;
#6957=CARTESIAN_POINT ( 'NONE',  ( 4.690415759823430619, 0.09999999999999982514, -4.500000000000000888 ) ) ;
#6960=PRODUCT_DEFINITION_FORMATION_WITH_SPECIFIED_SOURCE ( 'ANY', '', #1263, .NOT_KNOWN. ) ;
#6983=CARTESIAN_POINT ( 'NONE',  ( 2.525608486058770641, 2.900000000000000355, 2.423076923076923350 ) ) ;
#7011=ORIENTED_EDGE ( 'NONE', *, *, #3662, .F. ) ;
#7046=ADVANCED_FACE ( 'NONE', ( #1601 ), #7080, .T. ) ;
#7051=CARTESIAN_POINT ( 'NONE',  ( 0.000000000000000000, 0.1000000000000000056, -1.399999999999999911 ) ) ;
#7054=DIRECTION ( 'NONE',  ( 0.000000000000000000, 1.000000000000000000, -0.000000000000000000 ) ) ;
#7063=ORIENTED_EDGE ( 'NONE', *, *, #3527, .F. ) ;
#7073=DIRECTION ( 'NONE',  ( 0.000000000000000000, 0.000000000000000000, 1.000000000000000000 ) ) ;
#7080=TOROIDAL_SURFACE ( 'NONE', #10814, 1.600000000000000311, 0.1000000000000000056 ) ;
#7084=CARTESIAN_POINT ( 'NONE',  ( 4.225031457058369317E-16, 0.000000000000000000, -3.400000000000001243 ) ) ;
#7095=ORIENTED_EDGE ( 'NONE', *, *, #3705, .T. ) ;
#7096=DIRECTION ( 'NONE',  ( 0.000000000000000000, 0.000000000000000000, -1.000000000000000000 ) ) ;
#7117=FACE_BOUND ( 'NONE', #11114, .T. ) ;
#7118=ORIENTED_EDGE ( 'NONE', *, *, #3113, .F. ) ;
#7125=VECTOR ( 'NONE', #12569, 1000.000000000000000 ) ;
#7128=CARTESIAN_POINT ( 'NONE',  ( 4.690415759823430619, 2.900000000000000355, 1.500000000000000000 ) ) ;
#7138=DIRECTION ( 'NONE',  ( 0.000000000000000000, 0.000000000000000000, -1.000000000000000000 ) ) ;
#7143=VERTEX_POINT ( 'NONE', #13380 ) ;
#7159=ORIENTED_EDGE ( 'NONE', *, *, #10391, .T. ) ;
#7176=EDGE_CURVE ( 'NONE', #6069, #7533, #7302, .T. ) ;
#7187=EDGE_LOOP ( 'NONE', ( #1044, #6111, #255, #9127, #9249, #12773, #13301, #2981, #10733, #9508, #727, #8798 ) ) ;
#7194=DIRECTION ( 'NONE',  ( -1.000000000000000000, 0.000000000000000000, 0.000000000000000000 ) ) ;
#7208=ORIENTED_EDGE ( 'NONE', *, *, #864, .F. ) ;
#7221=EDGE_CURVE ( 'NONE', #11405, #10281, #2200, .T. ) ;
#7240=DIRECTION ( 'NONE',  ( 0.000000000000000000, 1.000000000000000000, -0.000000000000000000 ) ) ;
#7246=DIRECTION ( 'NONE',  ( -1.000000000000000000, -0.000000000000000000, -0.000000000000000000 ) ) ;
#7249=VERTEX_POINT ( 'NONE', #8594 ) ;
#7266=ADVANCED_FACE ( 'NONE', ( #5435 ), #11780, .T. ) ;
#7269=CIRCLE ( 'NONE', #3320, 3.500000000000000888 ) ;
#7274=DIRECTION ( 'NONE',  ( 0.000000000000000000, 0.000000000000000000, 1.000000000000000000 ) ) ;
#7287=ORIENTED_EDGE ( 'NONE', *, *, #4929, .F. ) ;
#7289=DIRECTION ( 'NONE',  ( 0.000000000000000000, 0.000000000000000000, -1.000000000000000000 ) ) ;
#7292=DIRECTION ( 'NONE',  ( 0.000000000000000000, 0.000000000000000000, 1.000000000000000000 ) ) ;
#7297=CYLINDRICAL_SURFACE ( 'NONE', #10204, 3.500000000000000888 ) ;
#7302=CIRCLE ( 'NONE', #3551, 3.499999999999999556 ) ;
#7304=FILL_AREA_STYLE ('',( #9498 ) ) ;
#7314=EDGE_LOOP ( 'NONE', ( #10400, #9403, #2535, #10312 ) ) ;
#7319=DIRECTION ( 'NONE',  ( -0.000000000000000000, -1.000000000000000000, -0.000000000000000000 ) ) ;
#7321=CIRCLE ( 'NONE', #8190, 0.1000000000000000472 ) ;
#7323=CARTESIAN_POINT ( 'NONE',  ( 4.690415759823430619, 0.000000000000000000, 4.500000000000000888 ) ) ;
#7341=FACE_OUTER_BOUND ( 'NONE', #2129, .T. ) ;
#7342=AXIS2_PLACEMENT_3D ( 'NONE', #9791, #11660, #11733 ) ;
#7351=CARTESIAN_POINT ( 'NONE',  ( 2.525608486058770641, 3.000000000000000000, 2.423076923076923350 ) ) ;
#7358=DIRECTION ( 'NONE',  ( -1.000000000000000000, -0.000000000000000000, -0.000000000000000000 ) ) ;
#7366=CARTESIAN_POINT ( 'NONE',  ( 0.000000000000000000, 3.000000000000000000, 1.500000000000000000 ) ) ;
#7375=ADVANCED_FACE ( 'NONE', ( #13014 ), #6207, .T. ) ;
#7377=SURFACE_STYLE_USAGE ( .BOTH. , #1036 ) ;
#7386=CIRCLE ( 'NONE', #12669, 3.500000000000000888 ) ;
#7411=CARTESIAN_POINT ( 'NONE',  ( 26.30958424017656938, 0.000000000000000000, -1.399999999999999911 ) ) ;
#7417=DIRECTION ( 'NONE',  ( 0.000000000000000000, 0.000000000000000000, -1.000000000000000000 ) ) ;
#7427=CARTESIAN_POINT ( 'NONE',  ( 28.54655175640005282, 3.000000000000000000, -2.353846153846155254 ) ) ;
#7433=ORIENTED_EDGE ( 'NONE', *, *, #1059, .T. ) ;
#7448=EDGE_CURVE ( 'NONE', #6498, #3500, #9510, .T. ) ;
#7455=CARTESIAN_POINT ( 'NONE',  ( 2.453448243599949397, 0.000000000000000000, -2.353846153846154365 ) ) ;
#7468=EDGE_LOOP ( 'NONE', ( #2427, #5678 ) ) ;
#7485=CARTESIAN_POINT ( 'NONE',  ( 0.000000000000000000, 3.000000000000000000, 0.000000000000000000 ) ) ;
#7503=CIRCLE ( 'NONE', #11437, 3.500000000000000888 ) ;
#7525=AXIS2_PLACEMENT_3D ( 'NONE', #2240, #7551, #3211 ) ;
#7527=LINE ( 'NONE', #11735, #13464 ) ;
#7533=VERTEX_POINT ( 'NONE', #685 ) ;
#7540=CYLINDRICAL_SURFACE ( 'NONE', #11555, 1.500000000000003997 ) ;
#7551=DIRECTION ( 'NONE',  ( 0.000000000000000000, 1.000000000000000000, -0.000000000000000000 ) ) ;
#7555=TOROIDAL_SURFACE ( 'NONE', #4924, 1.600000000000004086, 0.1000000000000000056 ) ;
#7586=AXIS2_PLACEMENT_3D ( 'NONE', #636, #4830, #7999 ) ;
#7595=CARTESIAN_POINT ( 'NONE',  ( 0.000000000000000000, 2.900000000000000355, 1.600000000000000311 ) ) ;
#7610=DIRECTION ( 'NONE',  ( -0.000000000000000000, -1.000000000000000000, -0.000000000000000000 ) ) ;
#7616=DIRECTION ( 'NONE',  ( 0.000000000000000000, 1.000000000000000000, -0.000000000000000000 ) ) ;
#7617=DIRECTION ( 'NONE',  ( 0.000000000000000000, 0.000000000000000000, 1.000000000000000000 ) ) ;
#7622=EDGE_LOOP ( 'NONE', ( #9780, #8896, #11358, #4579 ) ) ;
#7632=ORIENTED_EDGE ( 'NONE', *, *, #6041, .F. ) ;
#7634=EDGE_CURVE ( 'NONE', #9031, #6069, #1590, .T. ) ;
#7641=DIRECTION ( 'NONE',  ( 0.000000000000000000, 1.000000000000000000, -0.000000000000000000 ) ) ;
#7670=CARTESIAN_POINT ( 'NONE',  ( 28.47439151394123158, 0.09999999999999982514, -2.423076923076924682 ) ) ;
#7680=DIRECTION ( 'NONE',  ( 1.000000000000000000, 0.000000000000000000, 1.224646799147353207E-16 ) ) ;
#7715=AXIS2_PLACEMENT_3D ( 'NONE', #6713, #4371, #441 ) ;
#7732=FACE_OUTER_BOUND ( 'NONE', #8637, .T. ) ;
#7733=CLOSED_SHELL ( 'NONE', ( #3366, #10367, #4961, #1647, #6569, #1096, #7046, #5978, #7747, #9663, #9020, #10373, #7837, #13158, #1431, #7266, #2955, #3839, #11653, #11925, #8752, #6834, #8820, #10148, #11569, #537, #3461, #8431, #11959, #4724, #6500, #9462, #2260, #4227, #9962, #2465, #29, #7375, #9829, #11644, #10630, #2873, #9864, #11984, #4847, #13320, #12460, #2581, #10726, #12658 ) ) ;
#7747=ADVANCED_FACE ( 'NONE', ( #12856 ), #2905, .T. ) ;
#7751=AXIS2_PLACEMENT_3D ( 'NONE', #1502, #6534, #402 ) ;
#7767=ORIENTED_EDGE ( 'NONE', *, *, #4929, .T. ) ;
#7774=LINE ( 'NONE', #2546, #3393 ) ;
#7779=VERTEX_POINT ( 'NONE', #1759 ) ;
#7798=AXIS2_PLACEMENT_3D ( 'NONE', #11801, #9795, #11937 ) ;
#7808=CARTESIAN_POINT ( 'NONE',  ( 0.000000000000000000, 2.900000000000000355, 0.000000000000000000 ) ) ;
#7837=ADVANCED_FACE ( 'NONE', ( #3740 ), #6030, .F. ) ;
#7842=ORIENTED_EDGE ( 'NONE', *, *, #9921, .F. ) ;
#7844=ORIENTED_EDGE ( 'NONE', *, *, #4626, .F. ) ;
#7855=DIRECTION ( 'NONE',  ( 0.000000000000000000, 1.000000000000000000, -0.000000000000000000 ) ) ;
#7884=DIRECTION ( 'NONE',  ( 0.000000000000000000, 1.000000000000000000, -0.000000000000000000 ) ) ;
#7892=AXIS2_PLACEMENT_3D ( 'NONE', #4382, #2055, #4322 ) ;
#7901=DIRECTION ( 'NONE',  ( 0.000000000000000000, 0.000000000000000000, -1.000000000000000000 ) ) ;
#7905=AXIS2_PLACEMENT_3D ( 'NONE', #10512, #7616, #13549 ) ;
#7907=CIRCLE ( 'NONE', #9007, 3.100000000000000533 ) ;
#7912=ORIENTED_EDGE ( 'NONE', *, *, #458, .T. ) ;
#7916=APPLICATION_CONTEXT ( 'automotive_design' ) ;
#7926=DIRECTION ( 'NONE',  ( 0.000000000000000000, 0.000000000000000000, -1.000000000000000000 ) ) ;
#7939=SHAPE_REPRESENTATION ( 'link', ( #10007 ), #1673 ) ;
#7947=DIRECTION ( 'NONE',  ( 0.000000000000000000, 0.000000000000000000, -1.000000000000000000 ) ) ;
#7965=EDGE_LOOP ( 'NONE', ( #7159, #12966, #671, #2612 ) ) ;
#7969=ORIENTED_EDGE ( 'NONE', *, *, #9004, .T. ) ;
#7972=AXIS2_PLACEMENT_3D ( 'NONE', #576, #9101, #3869 ) ;
#7981=VECTOR ( 'NONE', #6261, 1000.000000000000000 ) ;
#7983=AXIS2_PLACEMENT_3D ( 'NONE', #1878, #5098, #13442 ) ;
#7991=DIRECTION ( 'NONE',  ( 0.000000000000000000, 0.000000000000000000, 1.000000000000000000 ) ) ;
#7992=TOROIDAL_SURFACE ( 'NONE', #749, 3.399999999999999911, 0.1000000000000000056 ) ;
#7993=CIRCLE ( 'NONE', #2064, 1.600000000000004086 ) ;
#7994=VECTOR ( 'NONE', #8238, 1000.000000000000000 ) ;
#7999=DIRECTION ( 'NONE',  ( 0.000000000000000000, 0.000000000000000000, 1.000000000000000000 ) ) ;
#8002=ORIENTED_EDGE ( 'NONE', *, *, #5571, .T. ) ;
#8013=DIRECTION ( 'NONE',  ( -0.000000000000000000, -1.000000000000000000, -0.000000000000000000 ) ) ;
#8014=CIRCLE ( 'NONE', #1198, 3.400000000000001243 ) ;
#8016=CIRCLE ( 'NONE', #4267, 0.1000000000000000472 ) ;
#8020=DIRECTION ( 'NONE',  ( 0.000000000000000000, 0.000000000000000000, 1.000000000000000000 ) ) ;
#8028=ORIENTED_EDGE ( 'NONE', *, *, #4678, .T. ) ;
#8032=DIRECTION ( 'NONE',  ( 0.000000000000000000, 1.000000000000000000, -0.000000000000000000 ) ) ;
#8039=CARTESIAN_POINT ( 'NONE',  ( 31.00000000000000000, 3.000000000000000000, 1.500000000000003997 ) ) ;
#8040=VERTEX_POINT ( 'NONE', #1400 ) ;
#8041=VERTEX_POINT ( 'NONE', #8549 ) ;
#8050=DIRECTION ( 'NONE',  ( 1.224646799147353207E-16, 0.000000000000000000, -1.000000000000000000 ) ) ;
#8061=DIRECTION ( 'NONE',  ( 0.000000000000000000, 0.000000000000000000, 1.000000000000000000 ) ) ;
#8066=DIRECTION ( 'NONE',  ( 0.000000000000000000, 0.000000000000000000, 1.000000000000000000 ) ) ;
#8070=DIRECTION ( 'NONE',  ( 0.000000000000000000, 0.000000000000000000, 1.000000000000000000 ) ) ;
#8072=FACE_OUTER_BOUND ( 'NONE', #11302, .T. ) ;
#8078=EDGE_LOOP ( 'NONE', ( #4464, #11497, #13321, #4805 ) ) ;
#8082=LINE ( 'NONE', #1956, #9460 ) ;
#8130=LINE ( 'NONE', #13577, #4257 ) ;
#8152=ORIENTED_EDGE ( 'NONE', *, *, #12581, .T. ) ;
#8160=DIRECTION ( 'NONE',  ( 0.000000000000000000, 0.000000000000000000, 1.000000000000000000 ) ) ;
#8164=FACE_OUTER_BOUND ( 'NONE', #323, .T. ) ;
#8172=EDGE_CURVE ( 'NONE', #7143, #3990, #7321, .T. ) ;
#8190=AXIS2_PLACEMENT_3D ( 'NONE', #2834, #4699, #7926 ) ;
#8194=CARTESIAN_POINT ( 'NONE',  ( 31.00000000000000000, 0.000000000000000000, 0.000000000000000000 ) ) ;
#8201=FACE_OUTER_BOUND ( 'NONE', #3321, .T. ) ;
#8204=EDGE_CURVE ( 'NONE', #8258, #3500, #9068, .T. ) ;
#8233=CARTESIAN_POINT ( 'NONE',  ( 0.000000000000000000, 2.900000000000000355, 0.000000000000000000 ) ) ;
#8238=DIRECTION ( 'NONE',  ( -0.000000000000000000, -1.000000000000000000, -0.000000000000000000 ) ) ;
#8239=AXIS2_PLACEMENT_3D ( 'NONE', #9399, #4094, #11532 ) ;
#8251=DIRECTION ( 'NONE',  ( 0.000000000000000000, 1.000000000000000000, -0.000000000000000000 ) ) ;
#8258=VERTEX_POINT ( 'NONE', #5720 ) ;
#8271=ORIENTED_EDGE ( 'NONE', *, *, #1033, .T. ) ;
#8272=EDGE_CURVE ( 'NONE', #10261, #2378, #10841, .T. ) ;
#8277=CARTESIAN_POINT ( 'NONE',  ( 31.00000000000000000, 3.000000000000000000, 0.000000000000000000 ) ) ;
#8292=ORIENTED_EDGE ( 'NONE', *, *, #3468, .F. ) ;
#8297=EDGE_CURVE ( 'NONE', #3277, #12193, #12612, .T. ) ;
#8308=DIRECTION ( 'NONE',  ( -0.000000000000000000, -1.000000000000000000, -0.000000000000000000 ) ) ;
#8321=DIRECTION ( 'NONE',  ( 0.000000000000000000, 0.000000000000000000, 1.000000000000000000 ) ) ;
#8334=EDGE_CURVE ( 'NONE', #3990, #6631, #9233, .T. ) ;
#8340=DIRECTION ( 'NONE',  ( -0.000000000000000000, -1.000000000000000000, 0.000000000000000000 ) ) ;
#8361=FACE_OUTER_BOUND ( 'NONE', #11503, .T. ) ;
#8385=EDGE_CURVE ( 'NONE', #13453, #11685, #12565, .T. ) ;
#8386=AXIS2_PLACEMENT_3D ( 'NONE', #2361, #4293, #5590 ) ;
#8395=EDGE_LOOP ( 'NONE', ( #626, #4596, #6546, #9066 ) ) ;
#8409=CARTESIAN_POINT ( 'NONE',  ( 1.959434878635765477E-16, 2.900000000000000355, -1.600000000000000311 ) ) ;
#8415=PLANE ( 'NONE',  #8239 ) ;
#8420=CIRCLE ( 'NONE', #9951, 3.100000000000000533 ) ;
#8429=AXIS2_PLACEMENT_3D ( 'NONE', #9181, #10977, #1547 ) ;
#8431=ADVANCED_FACE ( 'NONE', ( #8201 ), #12436, .F. ) ;
#8450=AXIS2_PLACEMENT_3D ( 'NONE', #2391, #8716, #3220 ) ;
#8459=VECTOR ( 'NONE', #7319, 1000.000000000000000 ) ;
#8467=DIRECTION ( 'NONE',  ( -0.000000000000000000, -1.000000000000000000, -0.000000000000000000 ) ) ;
#8472=AXIS2_PLACEMENT_3D ( 'NONE', #8576, #3349, #5554 ) ;
#8477=DIRECTION ( 'NONE',  ( 0.000000000000000000, 1.000000000000000000, -0.000000000000000000 ) ) ;
#8500=ORIENTED_EDGE ( 'NONE', *, *, #4550, .F. ) ;
#8505=ORIENTED_EDGE ( 'NONE', *, *, #9726, .T. ) ;
#8511=CARTESIAN_POINT ( 'NONE',  ( 4.690415759823430619, 2.900000000000000355, -4.500000000000000888 ) ) ;
#8528=DIRECTION ( 'NONE',  ( -0.000000000000000000, -1.000000000000000000, -0.000000000000000000 ) ) ;
#8542=DIRECTION ( 'NONE',  ( 0.000000000000000000, 0.000000000000000000, 1.000000000000000000 ) ) ;
#8548=ORIENTED_EDGE ( 'NONE', *, *, #11329, .T. ) ;
#8549=CARTESIAN_POINT ( 'NONE',  ( 0.000000000000000000, 2.900000000000000355, -3.500000000000000888 ) ) ;
#8554=TOROIDAL_SURFACE ( 'NONE', #9665, 1.600000000000000311, 0.1000000000000000056 ) ;
#8576=CARTESIAN_POINT ( 'NONE',  ( 0.000000000000000000, 2.900000000000000355, 0.000000000000000000 ) ) ;
#8581=ORIENTED_EDGE ( 'NONE', *, *, #11194, .F. ) ;
#8588=AXIS2_PLACEMENT_3D ( 'NONE', #2513, #3738, #12092 ) ;
#8594=CARTESIAN_POINT ( 'NONE',  ( 1.959434878635765477E-16, 3.000000000000000000, -1.600000000000000311 ) ) ;
#8603=CARTESIAN_POINT ( 'NONE',  ( 26.30958424017656938, 2.900000000000000355, -4.500000000000000888 ) ) ;
#8605=CARTESIAN_POINT ( 'NONE',  ( 31.00000000000000000, 0.09999999999999982514, 0.000000000000000000 ) ) ;
#8611=EDGE_CURVE ( 'NONE', #3201, #4927, #8796, .T. ) ;
#8618=EDGE_LOOP ( 'NONE', ( #12607, #3042, #6642, #12825 ) ) ;
#8637=EDGE_LOOP ( 'NONE', ( #225, #12502, #2907, #7844 ) ) ;
#8639=AXIS2_PLACEMENT_3D ( 'NONE', #3882, #6029, #4922 ) ;
#8641=VECTOR ( 'NONE', #10498, 1000.000000000000000 ) ;
#8649=DIRECTION ( 'NONE',  ( 0.000000000000000000, 0.000000000000000000, 1.000000000000000000 ) ) ;
#8673=ORIENTED_EDGE ( 'NONE', *, *, #5815, .T. ) ;
#8681=DIRECTION ( 'NONE',  ( 0.000000000000000000, 1.000000000000000000, -0.000000000000000000 ) ) ;
#8695=MECHANICAL_DESIGN_GEOMETRIC_PRESENTATION_REPRESENTATION('',(#12243),#1225);
#8702=FACE_OUTER_BOUND ( 'NONE', #10219, .T. ) ;
#8716=DIRECTION ( 'NONE',  ( -1.000000000000000000, 0.000000000000000000, 0.000000000000000000 ) ) ;
#8718=FACE_OUTER_BOUND ( 'NONE', #9141, .T. ) ;
#8722=EDGE_LOOP ( 'NONE', ( #5164, #4157, #1585, #4906 ) ) ;
#8730=DIRECTION ( 'NONE',  ( 0.000000000000000000, 0.000000000000000000, 1.000000000000000000 ) ) ;
#8733=CARTESIAN_POINT ( 'NONE',  ( 31.00000000000000000, 0.09999999999999982514, 1.500000000000003997 ) ) ;
#8752=ADVANCED_FACE ( 'NONE', ( #12341 ), #7297, .T. ) ;
#8782=ORIENTED_EDGE ( 'NONE', *, *, #5476, .F. ) ;
#8796=LINE ( 'NONE', #13017, #13492 ) ;
#8798=ORIENTED_EDGE ( 'NONE', *, *, #3643, .T. ) ;
#8802=VERTEX_POINT ( 'NONE', #6462 ) ;
#8803=VECTOR ( 'NONE', #7358, 1000.000000000000000 ) ;
#8809=DIRECTION ( 'NONE',  ( -0.000000000000000000, -1.000000000000000000, -0.000000000000000000 ) ) ;
#8819=AXIS2_PLACEMENT_3D ( 'NONE', #3819, #6778, #8020 ) ;
#8820=ADVANCED_FACE ( 'NONE', ( #8718 ), #9488, .F. ) ;
#8823=DIRECTION ( 'NONE',  ( -0.6923076923076927347, 0.000000000000000000, 0.7216024245882196597 ) ) ;
#8845=CARTESIAN_POINT ( 'NONE',  ( 28.54655175640005282, 2.900000000000000355, -2.353846153846155254 ) ) ;
#8849=CARTESIAN_POINT ( 'NONE',  ( 0.000000000000000000, 0.09999999999999982514, -1.500000000000000222 ) ) ;
#8856=CARTESIAN_POINT ( 'NONE',  ( 2.453448243599948952, 3.000000000000000000, -2.353846153846153921 ) ) ;
#8857=AXIS2_PLACEMENT_3D ( 'NONE', #4988, #12376, #12303 ) ;
#8860=EDGE_CURVE ( 'NONE', #3264, #8258, #12846, .T. ) ;
#8871=VERTEX_POINT ( 'NONE', #6941 ) ;
#8890=ORIENTED_EDGE ( 'NONE', *, *, #1030, .T. ) ;
#8893=AXIS2_PLACEMENT_3D ( 'NONE', #2497, #8809, #11736 ) ;
#8896=ORIENTED_EDGE ( 'NONE', *, *, #13504, .T. ) ;
#8910=EDGE_LOOP ( 'NONE', ( #8152, #8292, #6598, #3193 ) ) ;
#8913=ORIENTED_EDGE ( 'NONE', *, *, #5636, .F. ) ;
#8918=CARTESIAN_POINT ( 'NONE',  ( 31.00000000000000000, 3.000000000000000000, 3.499999999999999556 ) ) ;
#8919=CARTESIAN_POINT ( 'NONE',  ( 0.000000000000000000, 0.000000000000000000, 0.000000000000000000 ) ) ;
#8923=CARTESIAN_POINT ( 'NONE',  ( 4.163799117101002038E-16, 0.09999999999999982514, -3.400000000000001243 ) ) ;
#8939=DIRECTION ( 'NONE',  ( 0.000000000000000000, 1.000000000000000000, -0.000000000000000000 ) ) ;
#8951=DIRECTION ( 'NONE',  ( 0.000000000000000000, 1.000000000000000000, -0.000000000000000000 ) ) ;
#8966=LINE ( 'NONE', #11391, #121 ) ;
#8985=DIRECTION ( 'NONE',  ( -0.000000000000000000, -1.000000000000000000, 0.000000000000000000 ) ) ;
#8987=ORIENTED_EDGE ( 'NONE', *, *, #210, .F. ) ;
#9004=EDGE_CURVE ( 'NONE', #12045, #12265, #2941, .T. ) ;
#9007=AXIS2_PLACEMENT_3D ( 'NONE', #7323, #13461, #4016 ) ;
#9012=EDGE_LOOP ( 'NONE', ( #9386, #13344 ) ) ;
#9019=DIRECTION ( 'NONE',  ( -1.000000000000000000, 0.000000000000000000, 0.000000000000000000 ) ) ;
#9020=ADVANCED_FACE ( 'NONE', ( #8164 ), #2065, .T. ) ;
#9030=AXIS2_PLACEMENT_3D ( 'NONE', #9621, #3346, #2328 ) ;
#9031=VERTEX_POINT ( 'NONE', #3965 ) ;
#9061=EDGE_LOOP ( 'NONE', ( #13384, #1277, #11263, #8987 ) ) ;
#9066=ORIENTED_EDGE ( 'NONE', *, *, #4072, .T. ) ;
#9068=CIRCLE ( 'NONE', #10399, 3.500000000000000888 ) ;
#9073=DIRECTION ( 'NONE',  ( 1.000000000000000000, 0.000000000000000000, 1.224646799147353207E-16 ) ) ;
#9077=VECTOR ( 'NONE', #6053, 1000.000000000000000 ) ;
#9089=ORIENTED_EDGE ( 'NONE', *, *, #10984, .T. ) ;
#9099=DIRECTION ( 'NONE',  ( 0.000000000000000000, 0.000000000000000000, 1.000000000000000000 ) ) ;
#9101=DIRECTION ( 'NONE',  ( 0.000000000000000000, 1.000000000000000000, -0.000000000000000000 ) ) ;
#9105=AXIS2_PLACEMENT_3D ( 'NONE', #10961, #9019, #8070 ) ;
#9110=FACE_OUTER_BOUND ( 'NONE', #8910, .T. ) ;
#9117=CIRCLE ( 'NONE', #9562, 0.09999999999999982514 ) ;
#9127=ORIENTED_EDGE ( 'NONE', *, *, #2977, .T. ) ;
#9130=CIRCLE ( 'NONE', #5824, 0.09999999999999982514 ) ;
#9141=EDGE_LOOP ( 'NONE', ( #6672, #1744, #11772, #384 ) ) ;
#9152=CARTESIAN_POINT ( 'NONE',  ( 0.000000000000000000, 0.09999999999999982514, 0.000000000000000000 ) ) ;
#9168=CARTESIAN_POINT ( 'NONE',  ( 31.00000000000000000, 2.900000000000000355, 1.500000000000003997 ) ) ;
#9170=EDGE_LOOP ( 'NONE', ( #5035, #9089, #3172, #9374 ) ) ;
#9175=ORIENTED_EDGE ( 'NONE', *, *, #3341, .T. ) ;
#9181=CARTESIAN_POINT ( 'NONE',  ( 31.00000000000000000, 2.900000000000000355, 0.000000000000000000 ) ) ;
#9191=ORIENTED_EDGE ( 'NONE', *, *, #2977, .F. ) ;
#9195=DIRECTION ( 'NONE',  ( 0.6923076923076904032, -0.000000000000000000, 0.7216024245882218802 ) ) ;
#9197=LINE ( 'NONE', #8918, #11063 ) ;
#9233=LINE ( 'NONE', #13383, #2928 ) ;
#9235=EDGE_LOOP ( 'NONE', ( #10263, #10153, #12019, #4774 ) ) ;
#9238=AXIS2_PLACEMENT_3D ( 'NONE', #9245, #13462, #6220 ) ;
#9239=AXIS2_PLACEMENT_3D ( 'NONE', #11435, #2004, #11236 ) ;
#9245=CARTESIAN_POINT ( 'NONE',  ( 31.00000000000000000, 0.09999999999999982514, 0.000000000000000000 ) ) ;
#9249=ORIENTED_EDGE ( 'NONE', *, *, #3468, .T. ) ;
#9255=ORIENTED_EDGE ( 'NONE', *, *, #12656, .F. ) ;
#9282=EDGE_CURVE ( 'NONE', #3238, #10250, #493, .T. ) ;
#9283=AXIS2_PLACEMENT_3D ( 'NONE', #3467, #6641, #7617 ) ;
#9294=CARTESIAN_POINT ( 'NONE',  ( 26.30958424017656938, 0.000000000000000000, 4.500000000000000888 ) ) ;
#9299=( NAMED_UNIT ( * ) PLANE_ANGLE_UNIT ( ) SI_UNIT ( $, .RADIAN. ) );
#9301=CIRCLE ( 'NONE', #6667, 3.100000000000000533 ) ;
#9344=DIRECTION ( 'NONE',  ( 0.000000000000000000, 1.000000000000000000, -0.000000000000000000 ) ) ;
#9348=DIRECTION ( 'NONE',  ( 0.000000000000000000, 1.000000000000000000, -0.000000000000000000 ) ) ;
#9352=CARTESIAN_POINT ( 'NONE',  ( 0.000000000000000000, 0.09999999999999982514, 0.000000000000000000 ) ) ;
#9357=CARTESIAN_POINT ( 'NONE',  ( 31.00000000000000000, 2.900000000000000355, 0.000000000000000000 ) ) ;
#9363=DIRECTION ( 'NONE',  ( -0.000000000000000000, -1.000000000000000000, 0.000000000000000000 ) ) ;
#9370=EDGE_CURVE ( 'NONE', #4457, #9614, #10223, .T. ) ;
#9374=ORIENTED_EDGE ( 'NONE', *, *, #8204, .T. ) ;
#9375=DIRECTION ( 'NONE',  ( 0.000000000000000000, 1.000000000000000000, -0.000000000000000000 ) ) ;
#9386=ORIENTED_EDGE ( 'NONE', *, *, #10627, .T. ) ;
#9398=EDGE_CURVE ( 'NONE', #2521, #10261, #10827, .T. ) ;
#9399=CARTESIAN_POINT ( 'NONE',  ( 0.000000000000000000, 3.000000000000000000, -1.500000000000000000 ) ) ;
#9403=ORIENTED_EDGE ( 'NONE', *, *, #5665, .T. ) ;
#9410=CARTESIAN_POINT ( 'NONE',  ( 26.30958424017656938, 3.000000000000000000, 1.399999999999999911 ) ) ;
#9417=FACE_OUTER_BOUND ( 'NONE', #10796, .T. ) ;
#9422=DIRECTION ( 'NONE',  ( 0.000000000000000000, 0.000000000000000000, 1.000000000000000000 ) ) ;
#9447=CARTESIAN_POINT ( 'NONE',  ( 4.690415759823430619, 3.000000000000000000, -1.500000000000000000 ) ) ;
#9451=LINE ( 'NONE', #856, #8641 ) ;
#9460=VECTOR ( 'NONE', #1897, 1000.000000000000000 ) ;
#9462=ADVANCED_FACE ( 'NONE', ( #6556 ), #10840, .T. ) ;
#9479=VERTEX_POINT ( 'NONE', #1319 ) ;
#9488=PLANE ( 'NONE',  #11524 ) ;
#9490=EDGE_CURVE ( 'NONE', #7533, #4645, #3344, .T. ) ;
#9494=EDGE_LOOP ( 'NONE', ( #11774, #7063, #5455, #3871 ) ) ;
#9498=FILL_AREA_STYLE_COLOUR ( '', #10897 ) ;
#9508=ORIENTED_EDGE ( 'NONE', *, *, #1049, .T. ) ;
#9510=CIRCLE ( 'NONE', #10605, 0.09999999999999982514 ) ;
#9530=ORIENTED_EDGE ( 'NONE', *, *, #8611, .T. ) ;
#9543=DIRECTION ( 'NONE',  ( 0.000000000000000000, 0.000000000000000000, 1.000000000000000000 ) ) ;
#9545=DIRECTION ( 'NONE',  ( -0.000000000000000000, -1.000000000000000000, -0.000000000000000000 ) ) ;
#9551=EDGE_LOOP ( 'NONE', ( #1149, #3802, #9530, #11820 ) ) ;
#9559=FACE_OUTER_BOUND ( 'NONE', #1484, .T. ) ;
#9562=AXIS2_PLACEMENT_3D ( 'NONE', #5001, #9195, #1914 ) ;
#9565=EDGE_CURVE ( 'NONE', #10765, #1237, #10398, .T. ) ;
#9567=AXIS2_PLACEMENT_3D ( 'NONE', #790, #7194, #10423 ) ;
#9574=SHAPE_REPRESENTATION_RELATIONSHIP ( 'NONE' , 'NONE' ,  #7939, #3921 ) ;
#9585=ORIENTED_EDGE ( 'NONE', *, *, #5592, .F. ) ;
#9587=ORIENTED_EDGE ( 'NONE', *, *, #11489, .F. ) ;
#9614=VERTEX_POINT ( 'NONE', #11167 ) ;
#9621=CARTESIAN_POINT ( 'NONE',  ( 26.30958424017656938, 0.1000000000000000056, 1.399999999999999911 ) ) ;
#9624=EDGE_CURVE ( 'NONE', #12193, #12045, #4226, .T. ) ;
#9631=ORIENTED_EDGE ( 'NONE', *, *, #6943, .T. ) ;
#9634=CYLINDRICAL_SURFACE ( 'NONE', #12972, 3.500000000000000888 ) ;
#9663=ADVANCED_FACE ( 'NONE', ( #837 ), #5993, .T. ) ;
#9665=AXIS2_PLACEMENT_3D ( 'NONE', #5416, #5154, #65 ) ;
#9673=CIRCLE ( 'NONE', #665, 3.499999999999999556 ) ;
#9674=EDGE_LOOP ( 'NONE', ( #2112, #6293, #7632, #6618 ) ) ;
#9680=CIRCLE ( 'NONE', #3741, 3.000000000000000444 ) ;
#9683=FACE_BOUND ( 'NONE', #2141, .T. ) ;
#9690=EDGE_CURVE ( 'NONE', #12613, #3990, #5340, .T. ) ;
#9712=VECTOR ( 'NONE', #8467, 1000.000000000000000 ) ;
#9720=AXIS2_PLACEMENT_3D ( 'NONE', #6957, #8939, #12200 ) ;
#9726=EDGE_CURVE ( 'NONE', #12940, #12096, #10850, .T. ) ;
#9734=CYLINDRICAL_SURFACE ( 'NONE', #1209, 0.1000000000000000472 ) ;
#9738=AXIS2_PLACEMENT_3D ( 'NONE', #3690, #13205, #12113 ) ;
#9744=CARTESIAN_POINT ( 'NONE',  ( 31.00000000000000000, 2.900000000000000355, -1.600000000000004086 ) ) ;
#9745=ORIENTED_EDGE ( 'NONE', *, *, #4799, .T. ) ;
#9749=TOROIDAL_SURFACE ( 'NONE', #7342, 3.100000000000000533, 0.1000000000000000056 ) ;
#9771=AXIS2_PLACEMENT_3D ( 'NONE', #7051, #4490, #6488 ) ;
#9780=ORIENTED_EDGE ( 'NONE', *, *, #3438, .T. ) ;
#9782=CIRCLE ( 'NONE', #7586, 3.000000000000000888 ) ;
#9791=CARTESIAN_POINT ( 'NONE',  ( 4.690415759823430619, 2.900000000000000355, 4.500000000000000888 ) ) ;
#9795=DIRECTION ( 'NONE',  ( 0.000000000000000000, 1.000000000000000000, -0.000000000000000000 ) ) ;
#9802=ORIENTED_EDGE ( 'NONE', *, *, #9565, .T. ) ;
#9819=DIRECTION ( 'NONE',  ( 0.000000000000000000, 1.000000000000000000, -0.000000000000000000 ) ) ;
#9829=ADVANCED_FACE ( 'NONE', ( #5682 ), #6670, .T. ) ;
#9860=ORIENTED_EDGE ( 'NONE', *, *, #10209, .F. ) ;
#9864=ADVANCED_FACE ( 'NONE', ( #6722 ), #6654, .T. ) ;
#9881=DIRECTION ( 'NONE',  ( 0.000000000000000000, 0.000000000000000000, 1.000000000000000000 ) ) ;
#9883=DIRECTION ( 'NONE',  ( 0.7216024245882217691, 0.000000000000000000, 0.6923076923076904032 ) ) ;
#9892=ORIENTED_EDGE ( 'NONE', *, *, #8860, .T. ) ;
#9899=DIRECTION ( 'NONE',  ( 0.000000000000000000, 0.000000000000000000, 1.000000000000000000 ) ) ;
#9900=CARTESIAN_POINT ( 'NONE',  ( 31.00000000000000000, 0.09999999999999982514, 0.000000000000000000 ) ) ;
#9901=CARTESIAN_POINT ( 'NONE',  ( 0.000000000000000000, 0.09999999999999982514, 1.500000000000000000 ) ) ;
#9921=EDGE_CURVE ( 'NONE', #6069, #10765, #9197, .T. ) ;
#9929=DIRECTION ( 'NONE',  ( 1.000000000000000000, 0.000000000000000000, 0.000000000000000000 ) ) ;
#9944=AXIS2_PLACEMENT_3D ( 'NONE', #6091, #8340, #10287 ) ;
#9951=AXIS2_PLACEMENT_3D ( 'NONE', #9294, #4125, #13507 ) ;
#9962=ADVANCED_FACE ( 'NONE', ( #11062 ), #3141, .T. ) ;
#9984=CARTESIAN_POINT ( 'NONE',  ( 31.00000000000000000, 0.000000000000000000, 0.000000000000000000 ) ) ;
#9986=CIRCLE ( 'NONE', #2954, 1.500000000000003997 ) ;
#9993=CARTESIAN_POINT ( 'NONE',  ( 31.00000000000000000, 0.09999999999999982514, 3.499999999999999556 ) ) ;
#10007=AXIS2_PLACEMENT_3D ( 'NONE', #6754, #3381, #5712 ) ;
#10033=FACE_OUTER_BOUND ( 'NONE', #4458, .T. ) ;
#10038=ORIENTED_EDGE ( 'NONE', *, *, #1095, .F. ) ;
#10042=CARTESIAN_POINT ( 'NONE',  ( 31.00000000000000000, 3.000000000000000000, -1.600000000000004086 ) ) ;
#10048=DIRECTION ( 'NONE',  ( 0.000000000000000000, 0.000000000000000000, 1.000000000000000000 ) ) ;
#10076=DIRECTION ( 'NONE',  ( -1.000000000000000000, -0.000000000000000000, -0.000000000000000000 ) ) ;
#10116=CIRCLE ( 'NONE', #11881, 0.1000000000000000472 ) ;
#10123=FACE_OUTER_BOUND ( 'NONE', #5261, .T. ) ;
#10137=TOROIDAL_SURFACE ( 'NONE', #10577, 1.600000000000004086, 0.1000000000000000056 ) ;
#10139=CIRCLE ( 'NONE', #4416, 3.000000000000000888 ) ;
#10143=DIRECTION ( 'NONE',  ( -0.000000000000000000, -1.000000000000000000, -0.000000000000000000 ) ) ;
#10148=ADVANCED_FACE ( 'NONE', ( #7341 ), #12715, .F. ) ;
#10153=ORIENTED_EDGE ( 'NONE', *, *, #955, .T. ) ;
#10155=EDGE_LOOP ( 'NONE', ( #11783, #7208, #8782, #8913 ) ) ;
#10174=AXIS2_PLACEMENT_3D ( 'NONE', #8277, #3103, #11446 ) ;
#10175=AXIS2_PLACEMENT_3D ( 'NONE', #1351, #1491, #9881 ) ;
#10183=DIRECTION ( 'NONE',  ( 0.000000000000000000, 0.000000000000000000, -1.000000000000000000 ) ) ;
#10187=AXIS2_PLACEMENT_3D ( 'NONE', #6733, #3490, #5631 ) ;
#10201=VECTOR ( 'NONE', #8308, 1000.000000000000000 ) ;
#10204=AXIS2_PLACEMENT_3D ( 'NONE', #2063, #2885, #7096 ) ;
#10209=EDGE_CURVE ( 'NONE', #4931, #8802, #10642, .T. ) ;
#10219=EDGE_LOOP ( 'NONE', ( #8500, #5991, #3105, #1016 ) ) ;
#10223=LINE ( 'NONE', #9447, #5767 ) ;
#10250=VERTEX_POINT ( 'NONE', #4511 ) ;
#10257=DIRECTION ( 'NONE',  ( -0.000000000000000000, -1.000000000000000000, 0.000000000000000000 ) ) ;
#10261=VERTEX_POINT ( 'NONE', #2577 ) ;
#10263=ORIENTED_EDGE ( 'NONE', *, *, #10883, .T. ) ;
#10264=PRODUCT_DEFINITION_CONTEXT ( 'detailed design', #7916, 'design' ) ;
#10281=VERTEX_POINT ( 'NONE', #7670 ) ;
#10287=DIRECTION ( 'NONE',  ( 0.000000000000000000, 0.000000000000000000, 1.000000000000000000 ) ) ;
#10312=ORIENTED_EDGE ( 'NONE', *, *, #5905, .T. ) ;
#10325=ORIENTED_EDGE ( 'NONE', *, *, #5592, .T. ) ;
#10326=ORIENTED_EDGE ( 'NONE', *, *, #9565, .F. ) ;
#10344=CIRCLE ( 'NONE', #11888, 0.1000000000000001166 ) ;
#10366=CIRCLE ( 'NONE', #4865, 0.1000000000000000472 ) ;
#10367=ADVANCED_FACE ( 'NONE', ( #13395 ), #7555, .T. ) ;
#10373=ADVANCED_FACE ( 'NONE', ( #13256 ), #6680, .T. ) ;
#10384=TOROIDAL_SURFACE ( 'NONE', #10604, 3.400000000000001243, 0.1000000000000000056 ) ;
#10391=EDGE_CURVE ( 'NONE', #6347, #4645, #3154, .T. ) ;
#10395=VECTOR ( 'NONE', #5246, 1000.000000000000000 ) ;
#10397=DIRECTION ( 'NONE',  ( -0.6923076923076927347, 0.000000000000000000, 0.7216024245882196597 ) ) ;
#10398=CIRCLE ( 'NONE', #2915, 3.499999999999999556 ) ;
#10399=AXIS2_PLACEMENT_3D ( 'NONE', #12222, #12292, #5871 ) ;
#10400=ORIENTED_EDGE ( 'NONE', *, *, #9370, .T. ) ;
#10404=( LENGTH_UNIT ( ) NAMED_UNIT ( * ) SI_UNIT ( .MILLI., .METRE. ) );
#10407=AXIS2_PLACEMENT_3D ( 'NONE', #12805, #10797, #3425 ) ;
#10413=CARTESIAN_POINT ( 'NONE',  ( 4.690415759823430619, 3.000000000000000000, 1.399999999999999911 ) ) ;
#10415=DIRECTION ( 'NONE',  ( 0.000000000000000000, 0.000000000000000000, 1.000000000000000000 ) ) ;
#10421=AXIS2_PLACEMENT_3D ( 'NONE', #3126, #5064, #3065 ) ;
#10423=DIRECTION ( 'NONE',  ( 0.000000000000000000, 0.000000000000000000, 1.000000000000000000 ) ) ;
#10438=EDGE_CURVE ( 'NONE', #12045, #3201, #4035, .T. ) ;
#10476=EDGE_CURVE ( 'NONE', #2521, #7249, #5139, .T. ) ;
#10477=DIRECTION ( 'NONE',  ( -0.000000000000000000, -1.000000000000000000, 0.000000000000000000 ) ) ;
#10478=CARTESIAN_POINT ( 'NONE',  ( 4.690415759823430619, 3.000000000000000000, 4.500000000000000888 ) ) ;
#10483=CARTESIAN_POINT ( 'NONE',  ( 31.00000000000000000, 3.000000000000000000, 1.600000000000004086 ) ) ;
#10498=DIRECTION ( 'NONE',  ( -0.000000000000000000, -1.000000000000000000, -0.000000000000000000 ) ) ;
#10507=ORIENTED_EDGE ( 'NONE', *, *, #7634, .F. ) ;
#10512=CARTESIAN_POINT ( 'NONE',  ( 31.00000000000000000, 2.900000000000000355, 0.000000000000000000 ) ) ;
#10540=EDGE_CURVE ( 'NONE', #594, #3500, #9451, .T. ) ;
#10542=DIRECTION ( 'NONE',  ( 0.000000000000000000, 1.000000000000000000, -0.000000000000000000 ) ) ;
#10558=DIRECTION ( 'NONE',  ( 0.000000000000000000, 1.000000000000000000, -0.000000000000000000 ) ) ;
#10571=ORIENTED_EDGE ( 'NONE', *, *, #4306, .F. ) ;
#10574=EDGE_CURVE ( 'NONE', #4457, #7143, #997, .T. ) ;
#10577=AXIS2_PLACEMENT_3D ( 'NONE', #1084, #8251, #7292 ) ;
#10590=LINE ( 'NONE', #11485, #12982 ) ;
#10595=AXIS2_PLACEMENT_3D ( 'NONE', #6401, #8528, #12747 ) ;
#10599=ORIENTED_EDGE ( 'NONE', *, *, #2279, .F. ) ;
#10603=PRODUCT_DEFINITION ( 'UNKNOWN', '', #6960, #10264 ) ;
#10604=AXIS2_PLACEMENT_3D ( 'NONE', #9352, #6052, #4170 ) ;
#10605=AXIS2_PLACEMENT_3D ( 'NONE', #1659, #2750, #10048 ) ;
#10607=( NAMED_UNIT ( * ) SI_UNIT ( $, .STERADIAN. ) SOLID_ANGLE_UNIT ( ) );
#10622=CARTESIAN_POINT ( 'NONE',  ( 2.525608486058770641, 3.000000000000000000, -2.423076923076923350 ) ) ;
#10624=ORIENTED_EDGE ( 'NONE', *, *, #8611, .F. ) ;
#10627=EDGE_CURVE ( 'NONE', #12193, #3277, #7993, .T. ) ;
#10630=ADVANCED_FACE ( 'NONE', ( #10758 ), #9749, .T. ) ;
#10642=CIRCLE ( 'NONE', #10421, 3.100000000000000977 ) ;
#10648=( LENGTH_UNIT ( ) NAMED_UNIT ( * ) SI_UNIT ( .MILLI., .METRE. ) );
#10652=AXIS2_PLACEMENT_3D ( 'NONE', #3717, #1739, #13313 ) ;
#10662=AXIS2_PLACEMENT_3D ( 'NONE', #6587, #3348, #4326 ) ;
#10671=DIRECTION ( 'NONE',  ( 0.000000000000000000, 1.000000000000000000, -0.000000000000000000 ) ) ;
#10675=EDGE_LOOP ( 'NONE', ( #5482, #6566, #4757, #22 ) ) ;
#10676=FACE_OUTER_BOUND ( 'NONE', #11580, .T. ) ;
#10679=CARTESIAN_POINT ( 'NONE',  ( 4.690415759823430619, 0.000000000000000000, -4.500000000000000888 ) ) ;
#10697=DIRECTION ( 'NONE',  ( -0.000000000000000000, -1.000000000000000000, -0.000000000000000000 ) ) ;
#10706=ORIENTED_EDGE ( 'NONE', *, *, #11873, .T. ) ;
#10707=ORIENTED_EDGE ( 'NONE', *, *, #5828, .T. ) ;
#10715=DIRECTION ( 'NONE',  ( 0.000000000000000000, 1.000000000000000000, -0.000000000000000000 ) ) ;
#10726=ADVANCED_FACE ( 'NONE', ( #5387 ), #1414, .T. ) ;
#10733=ORIENTED_EDGE ( 'NONE', *, *, #9282, .T. ) ;
#10738=CARTESIAN_POINT ( 'NONE',  ( 0.000000000000000000, 3.000000000000000000, 0.000000000000000000 ) ) ;
#10751=EDGE_LOOP ( 'NONE', ( #6011, #9892, #9255, #9585 ) ) ;
#10758=FACE_OUTER_BOUND ( 'NONE', #4391, .T. ) ;
#10763=ORIENTED_EDGE ( 'NONE', *, *, #13504, .F. ) ;
#10765=VERTEX_POINT ( 'NONE', #9993 ) ;
#10783=EDGE_CURVE ( 'NONE', #12265, #1291, #11749, .T. ) ;
#10787=CARTESIAN_POINT ( 'NONE',  ( 31.00000000000000000, 2.900000000000000355, 3.499999999999999556 ) ) ;
#10792=AXIS2_PLACEMENT_3D ( 'NONE', #5910, #13424, #6876 ) ;
#10795=EDGE_LOOP ( 'NONE', ( #467, #7969, #3826, #10624 ) ) ;
#10796=EDGE_LOOP ( 'NONE', ( #2962, #1884, #7433, #630 ) ) ;
#10797=DIRECTION ( 'NONE',  ( 0.000000000000000000, 1.000000000000000000, -0.000000000000000000 ) ) ;
#10814=AXIS2_PLACEMENT_3D ( 'NONE', #1675, #5795, #13105 ) ;
#10825=AXIS2_PLACEMENT_3D ( 'NONE', #325, #6646, #4519 ) ;
#10827=CIRCLE ( 'NONE', #13264, 0.1000000000000000472 ) ;
#10836=VERTEX_POINT ( 'NONE', #2564 ) ;
#10840=TOROIDAL_SURFACE ( 'NONE', #4013, 3.399999999999999911, 0.1000000000000000056 ) ;
#10841=CIRCLE ( 'NONE', #7972, 1.500000000000000222 ) ;
#10850=CIRCLE ( 'NONE', #6004, 3.100000000000000533 ) ;
#10854=DIRECTION ( 'NONE',  ( -1.000000000000000000, 0.000000000000000000, 0.000000000000000000 ) ) ;
#10870=EDGE_LOOP ( 'NONE', ( #6780, #3578, #11715, #5852 ) ) ;
#10874=LINE ( 'NONE', #6595, #2488 ) ;
#10878=MECHANICAL_DESIGN_GEOMETRIC_PRESENTATION_REPRESENTATION('',(#5378),#4940);
#10883=EDGE_CURVE ( 'NONE', #2378, #10261, #761, .T. ) ;
#10897=COLOUR_RGB ( '',0.7803921568627451011, 0.7607843137254901578, 0.7411764705882353255 ) ;
#10939=DIRECTION ( 'NONE',  ( 0.000000000000000000, 0.000000000000000000, 1.000000000000000000 ) ) ;
#10954=EDGE_CURVE ( 'NONE', #4645, #13453, #8130, .T. ) ;
#10961=CARTESIAN_POINT ( 'NONE',  ( 31.00000000000000000, 0.09999999999999982514, 1.600000000000004086 ) ) ;
#10977=DIRECTION ( 'NONE',  ( 0.000000000000000000, 1.000000000000000000, -0.000000000000000000 ) ) ;
#10984=EDGE_CURVE ( 'NONE', #594, #8041, #11085, .T. ) ;
#10993=FACE_OUTER_BOUND ( 'NONE', #9494, .T. ) ;
#11000=AXIS2_PLACEMENT_3D ( 'NONE', #9900, #3637, #12053 ) ;
#11008=CARTESIAN_POINT ( 'NONE',  ( 4.690415759823430619, 0.09999999999999982514, -4.500000000000000888 ) ) ;
#11021=TOROIDAL_SURFACE ( 'NONE', #2015, 3.100000000000000977, 0.1000000000000000056 ) ;
#11062=FACE_OUTER_BOUND ( 'NONE', #12624, .T. ) ;
#11063=VECTOR ( 'NONE', #4934, 1000.000000000000000 ) ;
#11067=DIRECTION ( 'NONE',  ( 0.000000000000000000, 0.000000000000000000, 1.000000000000000000 ) ) ;
#11082=CARTESIAN_POINT ( 'NONE',  ( 26.30958424017656938, 0.09999999999999982514, -1.500000000000000000 ) ) ;
#11085=CIRCLE ( 'NONE', #2725, 3.500000000000000888 ) ;
#11101=DIRECTION ( 'NONE',  ( 0.000000000000000000, 0.000000000000000000, 1.000000000000000000 ) ) ;
#11111=EDGE_LOOP ( 'NONE', ( #804, #38, #4854, #6592 ) ) ;
#11114=EDGE_LOOP ( 'NONE', ( #1034, #9175 ) ) ;
#11153=LINE ( 'NONE', #9901, #6701 ) ;
#11165=FACE_OUTER_BOUND ( 'NONE', #4890, .T. ) ;
#11167=CARTESIAN_POINT ( 'NONE',  ( 4.690415759823430619, 0.09999999999999982514, -1.500000000000000000 ) ) ;
#11176=ORIENTED_EDGE ( 'NONE', *, *, #1033, .F. ) ;
#11180=CARTESIAN_POINT ( 'NONE',  ( 31.00000000000000000, 3.000000000000000000, -3.499999999999999556 ) ) ;
#11194=EDGE_CURVE ( 'NONE', #8041, #8258, #7774, .T. ) ;
#11203=CARTESIAN_POINT ( 'NONE',  ( 31.00000000000000000, 0.09999999999999982514, 0.000000000000000000 ) ) ;
#11206=EDGE_CURVE ( 'NONE', #11685, #4598, #11153, .T. ) ;
#11235=DIRECTION ( 'NONE',  ( 0.000000000000000000, 0.000000000000000000, 1.000000000000000000 ) ) ;
#11236=DIRECTION ( 'NONE',  ( 0.7216024245882196597, 0.000000000000000000, -0.6923076923076926237 ) ) ;
#11240=DIRECTION ( 'NONE',  ( 0.000000000000000000, 1.000000000000000000, -0.000000000000000000 ) ) ;
#11256=CARTESIAN_POINT ( 'NONE',  ( 26.30958424017656938, 2.900000000000000355, 1.399999999999999911 ) ) ;
#11263=ORIENTED_EDGE ( 'NONE', *, *, #1229, .F. ) ;
#11273=EDGE_CURVE ( 'NONE', #12695, #3555, #12862, .T. ) ;
#11302=EDGE_LOOP ( 'NONE', ( #3223, #7095, #10706, #12293, #11771, #8271, #12110, #8002, #7767, #8505, #3785, #6465 ) ) ;
#11308=CIRCLE ( 'NONE', #6461, 3.000000000000000888 ) ;
#11313=DIRECTION ( 'NONE',  ( 0.000000000000000000, 0.000000000000000000, 1.000000000000000000 ) ) ;
#11322=AXIS2_PLACEMENT_3D ( 'NONE', #5685, #3756, #12933 ) ;
#11329=EDGE_CURVE ( 'NONE', #12096, #13453, #8016, .T. ) ;
#11330=CARTESIAN_POINT ( 'NONE',  ( 0.000000000000000000, 3.000000000000000000, 0.000000000000000000 ) ) ;
#11338=VERTEX_POINT ( 'NONE', #3910 ) ;
#11341=CIRCLE ( 'NONE', #5388, 0.1000000000000000472 ) ;
#11356=LINE ( 'NONE', #7351, #9077 ) ;
#11358=ORIENTED_EDGE ( 'NONE', *, *, #5636, .T. ) ;
#11371=CARTESIAN_POINT ( 'NONE',  ( 1.836970198721030181E-16, 3.000000000000000000, 1.500000000000000222 ) ) ;
#11375=DIRECTION ( 'NONE',  ( -0.000000000000000000, -1.000000000000000000, 0.000000000000000000 ) ) ;
#11380=CARTESIAN_POINT ( 'NONE',  ( 26.30958424017656938, 3.000000000000000000, -4.500000000000000888 ) ) ;
#11391=CARTESIAN_POINT ( 'NONE',  ( 4.690415759823430619, 0.1000000000000000056, -1.500000000000000000 ) ) ;
#11392=EDGE_CURVE ( 'NONE', #12695, #8040, #6916, .T. ) ;
#11405=VERTEX_POINT ( 'NONE', #1026 ) ;
#11430=CARTESIAN_POINT ( 'NONE',  ( 4.690415759823430619, 3.000000000000000000, -4.500000000000000888 ) ) ;
#11435=CARTESIAN_POINT ( 'NONE',  ( 28.54655175640005282, 0.09999999999999982514, 2.353846153846154809 ) ) ;
#11437=AXIS2_PLACEMENT_3D ( 'NONE', #8233, #6045, #1844 ) ;
#11438=DIRECTION ( 'NONE',  ( 0.000000000000000000, 0.000000000000000000, 1.000000000000000000 ) ) ;
#11446=DIRECTION ( 'NONE',  ( 0.000000000000000000, 0.000000000000000000, -1.000000000000000000 ) ) ;
#11478=ORIENTED_EDGE ( 'NONE', *, *, #198, .T. ) ;
#11484=CARTESIAN_POINT ( 'NONE',  ( 28.47439151394123158, 3.000000000000000000, 2.423076923076924238 ) ) ;
#11485=CARTESIAN_POINT ( 'NONE',  ( 26.30958424017656938, 0.000000000000000000, -1.399999999999999911 ) ) ;
#11486=AXIS2_PLACEMENT_3D ( 'NONE', #9744, #7680, #7417 ) ;
#11487=SHAPE_DEFINITION_REPRESENTATION ( #13146, #7939 ) ;
#11489=EDGE_CURVE ( 'NONE', #3238, #10765, #2297, .T. ) ;
#11497=ORIENTED_EDGE ( 'NONE', *, *, #197, .T. ) ;
#11503=EDGE_LOOP ( 'NONE', ( #10507, #11478, #1425, #7118 ) ) ;
#11508=EDGE_CURVE ( 'NONE', #1584, #6704, #4942, .T. ) ;
#11521=VERTEX_POINT ( 'NONE', #11572 ) ;
#11524=AXIS2_PLACEMENT_3D ( 'NONE', #7366, #1231, #12801 ) ;
#11532=DIRECTION ( 'NONE',  ( -1.000000000000000000, 0.000000000000000000, -0.000000000000000000 ) ) ;
#11548=CARTESIAN_POINT ( 'NONE',  ( 28.47439151394123158, 0.09999999999999982514, 2.423076923076924238 ) ) ;
#11555=AXIS2_PLACEMENT_3D ( 'NONE', #2106, #7610, #3203 ) ;
#11557=ORIENTED_EDGE ( 'NONE', *, *, #1066, .F. ) ;
#11569=ADVANCED_FACE ( 'NONE', ( #10033 ), #2592, .T. ) ;
#11572=CARTESIAN_POINT ( 'NONE',  ( 28.54655175640005282, 3.000000000000000000, 2.353846153846155254 ) ) ;
#11580=EDGE_LOOP ( 'NONE', ( #5743, #13164, #2817, #3998 ) ) ;
#11592=LINE ( 'NONE', #10622, #10395 ) ;
#11613=DIRECTION ( 'NONE',  ( 0.000000000000000000, 1.000000000000000000, -0.000000000000000000 ) ) ;
#11644=ADVANCED_FACE ( 'NONE', ( #10993 ), #6472, .T. ) ;
#11653=ADVANCED_FACE ( 'NONE', ( #1641 ), #8415, .T. ) ;
#11656=DIRECTION ( 'NONE',  ( 0.000000000000000000, 0.000000000000000000, 1.000000000000000000 ) ) ;
#11660=DIRECTION ( 'NONE',  ( 0.000000000000000000, 1.000000000000000000, -0.000000000000000000 ) ) ;
#11664=CARTESIAN_POINT ( 'NONE',  ( 4.690415759823430619, 0.09999999999999982514, 1.500000000000000000 ) ) ;
#11673=DIRECTION ( 'NONE',  ( -0.000000000000000000, -1.000000000000000000, 0.000000000000000000 ) ) ;
#11674=CARTESIAN_POINT ( 'NONE',  ( 26.30958424017656938, 3.000000000000000000, 4.500000000000000888 ) ) ;
#11685=VERTEX_POINT ( 'NONE', #11664 ) ;
#11690=CARTESIAN_POINT ( 'NONE',  ( 0.000000000000000000, 0.000000000000000000, 1.399999999999999911 ) ) ;
#11700=ORIENTED_EDGE ( 'NONE', *, *, #3801, .T. ) ;
#11712=ORIENTED_EDGE ( 'NONE', *, *, #2446, .F. ) ;
#11715=ORIENTED_EDGE ( 'NONE', *, *, #8172, .F. ) ;
#11733=DIRECTION ( 'NONE',  ( 0.000000000000000000, 0.000000000000000000, 1.000000000000000000 ) ) ;
#11735=CARTESIAN_POINT ( 'NONE',  ( 26.30958424017656938, 3.000000000000000000, 1.500000000000000000 ) ) ;
#11736=DIRECTION ( 'NONE',  ( 0.000000000000000000, 0.000000000000000000, -1.000000000000000000 ) ) ;
#11749=CIRCLE ( 'NONE', #9105, 0.1000000000000000472 ) ;
#11766=CIRCLE ( 'NONE', #4066, 3.499999999999999556 ) ;
#11771=ORIENTED_EDGE ( 'NONE', *, *, #8334, .T. ) ;
#11772=ORIENTED_EDGE ( 'NONE', *, *, #6943, .F. ) ;
#11774=ORIENTED_EDGE ( 'NONE', *, *, #11273, .F. ) ;
#11780=CYLINDRICAL_SURFACE ( 'NONE', #10595, 3.499999999999999556 ) ;
#11783=ORIENTED_EDGE ( 'NONE', *, *, #11960, .F. ) ;
#11798=FACE_OUTER_BOUND ( 'NONE', #9170, .T. ) ;
#11801=CARTESIAN_POINT ( 'NONE',  ( 31.00000000000000000, 3.000000000000000000, 0.000000000000000000 ) ) ;
#11817=DIRECTION ( 'NONE',  ( 0.000000000000000000, 0.000000000000000000, 1.000000000000000000 ) ) ;
#11820=ORIENTED_EDGE ( 'NONE', *, *, #13209, .T. ) ;
#11862=DIRECTION ( 'NONE',  ( -0.000000000000000000, -1.000000000000000000, 0.000000000000000000 ) ) ;
#11873=EDGE_CURVE ( 'NONE', #937, #12613, #6927, .T. ) ;
#11881=AXIS2_PLACEMENT_3D ( 'NONE', #8409, #229, #3186 ) ;
#11888=AXIS2_PLACEMENT_3D ( 'NONE', #2635, #8823, #2781 ) ;
#11908=EDGE_CURVE ( 'NONE', #13228, #10765, #11766, .T. ) ;
#11925=ADVANCED_FACE ( 'NONE', ( #3516 ), #4623, .F. ) ;
#11933=AXIS2_PLACEMENT_3D ( 'NONE', #12006, #5927, #6694 ) ;
#11937=DIRECTION ( 'NONE',  ( 0.000000000000000000, 0.000000000000000000, 1.000000000000000000 ) ) ;
#11958=ORIENTED_EDGE ( 'NONE', *, *, #9726, .F. ) ;
#11959=ADVANCED_FACE ( 'NONE', ( #8072, #3928, #7117 ), #2692, .T. ) ;
#11960=EDGE_CURVE ( 'NONE', #6054, #1237, #9130, .T. ) ;
#11968=DIRECTION ( 'NONE',  ( 0.000000000000000000, 1.000000000000000000, -0.000000000000000000 ) ) ;
#11981=DIRECTION ( 'NONE',  ( -0.000000000000000000, -1.000000000000000000, -0.000000000000000000 ) ) ;
#11984=ADVANCED_FACE ( 'NONE', ( #1676 ), #336, .T. ) ;
#11992=DIRECTION ( 'NONE',  ( -0.000000000000000000, -1.000000000000000000, -0.000000000000000000 ) ) ;
#12006=CARTESIAN_POINT ( 'NONE',  ( 31.00000000000000000, 2.900000000000000355, 1.600000000000004086 ) ) ;
#12019=ORIENTED_EDGE ( 'NONE', *, *, #3527, .T. ) ;
#12035=DIRECTION ( 'NONE',  ( 0.000000000000000000, 0.000000000000000000, 1.000000000000000000 ) ) ;
#12045=VERTEX_POINT ( 'NONE', #9168 ) ;
#12051=EDGE_CURVE ( 'NONE', #6704, #11685, #9782, .T. ) ;
#12053=DIRECTION ( 'NONE',  ( 0.000000000000000000, 0.000000000000000000, 1.000000000000000000 ) ) ;
#12075=CARTESIAN_POINT ( 'NONE',  ( 31.00000000000000000, 0.09999999999999982514, -3.399999999999999911 ) ) ;
#12092=DIRECTION ( 'NONE',  ( 0.000000000000000000, 0.000000000000000000, 1.000000000000000000 ) ) ;
#12095=ORIENTED_EDGE ( 'NONE', *, *, #1543, .F. ) ;
#12096=VERTEX_POINT ( 'NONE', #10413 ) ;
#12110=ORIENTED_EDGE ( 'NONE', *, *, #1066, .T. ) ;
#12113=DIRECTION ( 'NONE',  ( 0.000000000000000000, 0.000000000000000000, 1.000000000000000000 ) ) ;
#12117=ORIENTED_EDGE ( 'NONE', *, *, #5476, .T. ) ;
#12122=DIRECTION ( 'NONE',  ( 1.000000000000000000, 0.000000000000000000, 0.000000000000000000 ) ) ;
#12123=CIRCLE ( 'NONE', #12354, 3.000000000000000888 ) ;
#12159=CARTESIAN_POINT ( 'NONE',  ( 4.286263797015737088E-16, 0.09999999999999982514, 3.500000000000000888 ) ) ;
#12160=LINE ( 'NONE', #2576, #2642 ) ;
#12177=AXIS2_PLACEMENT_3D ( 'NONE', #3355, #343, #4334 ) ;
#12193=VERTEX_POINT ( 'NONE', #10483 ) ;
#12200=DIRECTION ( 'NONE',  ( 0.000000000000000000, 0.000000000000000000, 1.000000000000000000 ) ) ;
#12211=VERTEX_POINT ( 'NONE', #17 ) ;
#12222=CARTESIAN_POINT ( 'NONE',  ( 0.000000000000000000, 0.09999999999999982514, 0.000000000000000000 ) ) ;
#12243=STYLED_ITEM ( 'NONE', ( #1168 ), #3921 ) ;
#12265=VERTEX_POINT ( 'NONE', #8733 ) ;
#12290=CARTESIAN_POINT ( 'NONE',  ( 0.000000000000000000, 3.000000000000000000, 0.000000000000000000 ) ) ;
#12292=DIRECTION ( 'NONE',  ( 0.000000000000000000, 1.000000000000000000, -0.000000000000000000 ) ) ;
#12293=ORIENTED_EDGE ( 'NONE', *, *, #9690, .T. ) ;
#12303=DIRECTION ( 'NONE',  ( 0.000000000000000000, 0.000000000000000000, 1.000000000000000000 ) ) ;
#12331=CARTESIAN_POINT ( 'NONE',  ( 31.00000000000000000, 2.900000000000000355, -1.500000000000003997 ) ) ;
#12341=FACE_OUTER_BOUND ( 'NONE', #5055, .T. ) ;
#12354=AXIS2_PLACEMENT_3D ( 'NONE', #1785, #10257, #552 ) ;
#12369=ORIENTED_EDGE ( 'NONE', *, *, #12656, .T. ) ;
#12373=DIRECTION ( 'NONE',  ( -0.000000000000000000, -1.000000000000000000, -0.000000000000000000 ) ) ;
#12376=DIRECTION ( 'NONE',  ( 0.000000000000000000, 1.000000000000000000, -0.000000000000000000 ) ) ;
#12411=DIRECTION ( 'NONE',  ( 0.000000000000000000, 0.000000000000000000, 1.000000000000000000 ) ) ;
#12412=EDGE_CURVE ( 'NONE', #4927, #11338, #11341, .T. ) ;
#12423=CARTESIAN_POINT ( 'NONE',  ( 2.453448243599948952, 2.900000000000000355, 2.353846153846153921 ) ) ;
#12426=DIRECTION ( 'NONE',  ( -0.000000000000000000, -1.000000000000000000, 0.000000000000000000 ) ) ;
#12436=CYLINDRICAL_SURFACE ( 'NONE', #6017, 3.000000000000000888 ) ;
#12456=ORIENTED_EDGE ( 'NONE', *, *, #12412, .T. ) ;
#12460=ADVANCED_FACE ( 'NONE', ( #6319 ), #4517, .T. ) ;
#12468=FACE_OUTER_BOUND ( 'NONE', #7965, .T. ) ;
#12487=CARTESIAN_POINT ( 'NONE',  ( 31.00000000000000000, 3.000000000000000000, -3.399999999999999911 ) ) ;
#12494=CARTESIAN_POINT ( 'NONE',  ( 26.30958424017656938, 3.000000000000000000, -1.399999999999999911 ) ) ;
#12502=ORIENTED_EDGE ( 'NONE', *, *, #11206, .F. ) ;
#12551=CARTESIAN_POINT ( 'NONE',  ( 0.000000000000000000, 2.900000000000000355, 0.000000000000000000 ) ) ;
#12565=LINE ( 'NONE', #1253, #8459 ) ;
#12569=DIRECTION ( 'NONE',  ( 1.000000000000000000, 0.000000000000000000, 0.000000000000000000 ) ) ;
#12570=CARTESIAN_POINT ( 'NONE',  ( 2.525608486058770641, 0.09999999999999982514, 2.423076923076923350 ) ) ;
#12581=EDGE_CURVE ( 'NONE', #5856, #4931, #3856, .T. ) ;
#12585=CIRCLE ( 'NONE', #8588, 3.100000000000000533 ) ;
#12587=CARTESIAN_POINT ( 'NONE',  ( 31.00000000000000000, 0.09999999999999982514, -1.500000000000003997 ) ) ;
#12607=ORIENTED_EDGE ( 'NONE', *, *, #5411, .T. ) ;
#12612=CIRCLE ( 'NONE', #6656, 1.600000000000004086 ) ;
#12613=VERTEX_POINT ( 'NONE', #7427 ) ;
#12624=EDGE_LOOP ( 'NONE', ( #12950, #6792, #12908, #2461 ) ) ;
#12656=EDGE_CURVE ( 'NONE', #12211, #8258, #7386, .T. ) ;
#12658=ADVANCED_FACE ( 'NONE', ( #6382 ), #6716, .T. ) ;
#12667=DIRECTION ( 'NONE',  ( -0.000000000000000000, -1.000000000000000000, 0.000000000000000000 ) ) ;
#12669=AXIS2_PLACEMENT_3D ( 'NONE', #202, #10671, #5421 ) ;
#12695=VERTEX_POINT ( 'NONE', #8849 ) ;
#12702=CARTESIAN_POINT ( 'NONE',  ( 0.000000000000000000, 3.000000000000000000, 0.000000000000000000 ) ) ;
#12715=CYLINDRICAL_SURFACE ( 'NONE', #1391, 3.000000000000000888 ) ;
#12723=EDGE_CURVE ( 'NONE', #1584, #6498, #8014, .T. ) ;
#12747=DIRECTION ( 'NONE',  ( 0.000000000000000000, 0.000000000000000000, -1.000000000000000000 ) ) ;
#12753=AXIS2_PLACEMENT_3D ( 'NONE', #6266, #10477, #1035 ) ;
#12760=TOROIDAL_SURFACE ( 'NONE', #7905, 3.399999999999999911, 0.1000000000000000056 ) ;
#12762=DIRECTION ( 'NONE',  ( 0.000000000000000000, 0.000000000000000000, -1.000000000000000000 ) ) ;
#12773=ORIENTED_EDGE ( 'NONE', *, *, #10209, .T. ) ;
#12801=DIRECTION ( 'NONE',  ( -1.000000000000000000, 0.000000000000000000, -0.000000000000000000 ) ) ;
#12805=CARTESIAN_POINT ( 'NONE',  ( 0.000000000000000000, 3.000000000000000000, 0.000000000000000000 ) ) ;
#12825=ORIENTED_EDGE ( 'NONE', *, *, #10574, .T. ) ;
#12829=CIRCLE ( 'NONE', #10187, 1.600000000000004086 ) ;
#12846=CIRCLE ( 'NONE', #312, 0.09999999999999982514 ) ;
#12847=AXIS2_PLACEMENT_3D ( 'NONE', #645, #13113, #3524 ) ;
#12856=FACE_OUTER_BOUND ( 'NONE', #10751, .T. ) ;
#12862=CIRCLE ( 'NONE', #2736, 0.1000000000000000472 ) ;
#12872=CARTESIAN_POINT ( 'NONE',  ( 26.30958424017656938, 0.09999999999999982514, -1.399999999999999467 ) ) ;
#12897=EDGE_CURVE ( 'NONE', #3201, #12045, #9986, .T. ) ;
#12908=ORIENTED_EDGE ( 'NONE', *, *, #11508, .F. ) ;
#12933=DIRECTION ( 'NONE',  ( 0.000000000000000000, 0.000000000000000000, -1.000000000000000000 ) ) ;
#12940=VERTEX_POINT ( 'NONE', #4587 ) ;
#12950=ORIENTED_EDGE ( 'NONE', *, *, #6482, .T. ) ;
#12954=ORIENTED_EDGE ( 'NONE', *, *, #5411, .F. ) ;
#12966=ORIENTED_EDGE ( 'NONE', *, *, #9490, .F. ) ;
#12972=AXIS2_PLACEMENT_3D ( 'NONE', #10738, #2134, #211 ) ;
#12981=AXIS2_PLACEMENT_3D ( 'NONE', #13258, #2637, #6844 ) ;
#12982=VECTOR ( 'NONE', #5217, 1000.000000000000000 ) ;
#13007=EDGE_LOOP ( 'NONE', ( #2175, #2821, #3580, #1520 ) ) ;
#13012=CARTESIAN_POINT ( 'NONE',  ( 26.30958424017656938, 0.09999999999999982514, -4.500000000000000888 ) ) ;
#13014=FACE_OUTER_BOUND ( 'NONE', #5781, .T. ) ;
#13017=CARTESIAN_POINT ( 'NONE',  ( 31.00000000000000000, 3.000000000000000000, -1.500000000000003997 ) ) ;
#13041=AXIS2_PLACEMENT_3D ( 'NONE', #4524, #9819, #392 ) ;
#13067=CARTESIAN_POINT ( 'NONE',  ( 31.00000000000000000, 0.000000000000000000, -3.399999999999999911 ) ) ;
#13105=DIRECTION ( 'NONE',  ( 0.000000000000000000, 0.000000000000000000, 1.000000000000000000 ) ) ;
#13106=DIRECTION ( 'NONE',  ( 0.000000000000000000, 0.000000000000000000, -1.000000000000000000 ) ) ;
#13113=DIRECTION ( 'NONE',  ( 0.000000000000000000, 1.000000000000000000, -0.000000000000000000 ) ) ;
#13116=CARTESIAN_POINT ( 'NONE',  ( 0.000000000000000000, 0.09999999999999982514, 0.000000000000000000 ) ) ;
#13120=DIRECTION ( 'NONE',  ( -0.000000000000000000, -1.000000000000000000, 0.000000000000000000 ) ) ;
#13121=CARTESIAN_POINT ( 'NONE',  ( 4.690415759823430619, 3.000000000000000000, -1.399999999999999911 ) ) ;
#13123=DIRECTION ( 'NONE',  ( -0.000000000000000000, -1.000000000000000000, -0.000000000000000000 ) ) ;
#13133=CARTESIAN_POINT ( 'NONE',  ( 0.000000000000000000, 0.09999999999999982514, 0.000000000000000000 ) ) ;
#13142=EDGE_CURVE ( 'NONE', #11521, #7533, #9117, .T. ) ;
#13144=CARTESIAN_POINT ( 'NONE',  ( 31.00000000000000000, 2.900000000000000355, 3.399999999999999911 ) ) ;
#13146=PRODUCT_DEFINITION_SHAPE ( 'NONE', 'NONE',  #10603 ) ;
#13158=ADVANCED_FACE ( 'NONE', ( #3004 ), #7540, .F. ) ;
#13164=ORIENTED_EDGE ( 'NONE', *, *, #10984, .F. ) ;
#13175=ORIENTED_EDGE ( 'NONE', *, *, #2823, .F. ) ;
#13189=EDGE_LOOP ( 'NONE', ( #6550, #4142, #11557, #5228 ) ) ;
#13201=DIRECTION ( 'NONE',  ( 1.224646799147353454E-16, 0.000000000000000000, -1.000000000000000000 ) ) ;
#13205=DIRECTION ( 'NONE',  ( 0.000000000000000000, 1.000000000000000000, -0.000000000000000000 ) ) ;
#13209=EDGE_CURVE ( 'NONE', #4927, #12265, #548, .T. ) ;
#13217=TOROIDAL_SURFACE ( 'NONE', #4195, 3.100000000000000977, 0.1000000000000000056 ) ;
#13227=MANIFOLD_SOLID_BREP ( 'Fillet1', #7733 ) ;
#13228=VERTEX_POINT ( 'NONE', #11548 ) ;
#13243=EDGE_LOOP ( 'NONE', ( #6884, #4409, #377, #3015 ) ) ;
#13249=CYLINDRICAL_SURFACE ( 'NONE', #5746, 0.1000000000000000472 ) ;
#13256=FACE_OUTER_BOUND ( 'NONE', #8395, .T. ) ;
#13258=CARTESIAN_POINT ( 'NONE',  ( 2.453448243599948952, 2.900000000000000355, -2.353846153846153921 ) ) ;
#13261=CARTESIAN_POINT ( 'NONE',  ( 0.000000000000000000, 3.000000000000000000, 0.000000000000000000 ) ) ;
#13264=AXIS2_PLACEMENT_3D ( 'NONE', #7595, #1254, #8542 ) ;
#13275=CARTESIAN_POINT ( 'NONE',  ( 26.30958424017656938, 2.900000000000000355, 4.500000000000000888 ) ) ;
#13276=DIRECTION ( 'NONE',  ( 0.000000000000000000, 0.000000000000000000, -1.000000000000000000 ) ) ;
#13283=CIRCLE ( 'NONE', #8639, 0.09999999999999982514 ) ;
#13299=UNCERTAINTY_MEASURE_WITH_UNIT (LENGTH_MEASURE( 1.000000000000000082E-05 ), #10404, 'distance_accuracy_value', 'NONE');
#13301=ORIENTED_EDGE ( 'NONE', *, *, #864, .T. ) ;
#13308=AXIS2_PLACEMENT_3D ( 'NONE', #8603, #8477, #4207 ) ;
#13313=DIRECTION ( 'NONE',  ( 0.000000000000000000, 0.000000000000000000, 1.000000000000000000 ) ) ;
#13320=ADVANCED_FACE ( 'NONE', ( #2574 ), #9734, .T. ) ;
#13321=ORIENTED_EDGE ( 'NONE', *, *, #10438, .F. ) ;
#13328=CYLINDRICAL_SURFACE ( 'NONE', #9771, 0.1000000000000000472 ) ;
#13344=ORIENTED_EDGE ( 'NONE', *, *, #8297, .T. ) ;
#13347=CARTESIAN_POINT ( 'NONE',  ( 4.690415759823430619, 2.900000000000000355, 4.500000000000000888 ) ) ;
#13380=CARTESIAN_POINT ( 'NONE',  ( 26.30958424017656938, 2.900000000000000355, -1.500000000000000000 ) ) ;
#13383=CARTESIAN_POINT ( 'NONE',  ( 0.000000000000000000, 3.000000000000000000, -1.399999999999999911 ) ) ;
#13384=ORIENTED_EDGE ( 'NONE', *, *, #11392, .F. ) ;
#13395=FACE_OUTER_BOUND ( 'NONE', #8078, .T. ) ;
#13411=EDGE_CURVE ( 'NONE', #5856, #9614, #8966, .T. ) ;
#13421=CIRCLE ( 'NONE', #3512, 1.500000000000000222 ) ;
#13424=DIRECTION ( 'NONE',  ( -1.000000000000000000, -0.000000000000000000, -0.000000000000000000 ) ) ;
#13442=DIRECTION ( 'NONE',  ( -3.357529308342206122E-15, 0.000000000000000000, 1.000000000000000000 ) ) ;
#13444=CIRCLE ( 'NONE', #1561, 3.000000000000000888 ) ;
#13453=VERTEX_POINT ( 'NONE', #7128 ) ;
#13459=CARTESIAN_POINT ( 'NONE',  ( 26.30958424017656938, 0.000000000000000000, 1.399999999999999911 ) ) ;
#13461=DIRECTION ( 'NONE',  ( 0.000000000000000000, 1.000000000000000000, -0.000000000000000000 ) ) ;
#13462=DIRECTION ( 'NONE',  ( 0.000000000000000000, 1.000000000000000000, -0.000000000000000000 ) ) ;
#13463=CARTESIAN_POINT ( 'NONE',  ( 0.000000000000000000, 2.900000000000000355, -1.500000000000000000 ) ) ;
#13464=VECTOR ( 'NONE', #2292, 1000.000000000000000 ) ;
#13487=ORIENTED_EDGE ( 'NONE', *, *, #8172, .T. ) ;
#13488=CIRCLE ( 'NONE', #9738, 1.600000000000000311 ) ;
#13492=VECTOR ( 'NONE', #5915, 1000.000000000000000 ) ;
#13504=EDGE_CURVE ( 'NONE', #9031, #1237, #5114, .T. ) ;
#13507=DIRECTION ( 'NONE',  ( 0.000000000000000000, 0.000000000000000000, 1.000000000000000000 ) ) ;
#13544=ORIENTED_EDGE ( 'NONE', *, *, #11908, .T. ) ;
#13549=DIRECTION ( 'NONE',  ( 0.000000000000000000, 0.000000000000000000, 1.000000000000000000 ) ) ;
#13560=DIRECTION ( 'NONE',  ( -0.000000000000000000, -1.000000000000000000, -0.000000000000000000 ) ) ;
#13577=CARTESIAN_POINT ( 'NONE',  ( 4.690415759823430619, 2.900000000000000355, 1.500000000000000000 ) ) ;
#13587=CYLINDRICAL_SURFACE ( 'NONE', #10174, 1.500000000000003997 ) ;
#13629=COLOUR_RGB('Light Blue',0.38,0.62,0.78);
#13630=FILL_AREA_STYLE_COLOUR('',#13629);
#13631=FILL_AREA_STYLE('',(#13630));
#13632=SURFACE_STYLE_FILL_AREA(#13631);
#13633=SURFACE_SIDE_STYLE('',(#13632));
#13634=SURFACE_STYLE_USAGE(.BOTH.,#13633);
#13635=PRESENTATION_STYLE_ASSIGNMENT((#13634));
ENDSEC;
END-ISO-10303-21;
